ISO-10303-21;
HEADER;
/* Generated by software containing ST-Developer
 * from STEP Tools, Inc. (www.steptools.com) 
 */

FILE_DESCRIPTION(
/* description */ (''),
/* implementation_level */ '2;1');

FILE_NAME(
/* name */ 'ISO 4026 - M3 x 4 - 45H (Bush Retaining Screw).step',
/* time_stamp */ '2026-10-05T09:57:53+05:00',
/* author */ (''),
/* organization */ (''),
/* preprocessor_version */ 'ST-DEVELOPER v20.2',
/* originating_system */ 'Autodesk Translation Framework v15.15.0.0',
/* authorisation */ '');

FILE_SCHEMA (('AUTOMOTIVE_DESIGN { 1 0 10303 214 3 1 1 }'));
ENDSEC;

DATA;
#10=MECHANICAL_DESIGN_GEOMETRIC_PRESENTATION_REPRESENTATION('',(#565),#113984);
#419=(
BOUNDED_CURVE()
B_SPLINE_CURVE(2,(#109503,#109504,#109505),.UNSPECIFIED.,.F.,.F.)
B_SPLINE_CURVE_WITH_KNOTS((3,3),(0.,0.0160544451505045),.UNSPECIFIED.)
CURVE()
GEOMETRIC_REPRESENTATION_ITEM()
RATIONAL_B_SPLINE_CURVE((1.,1.02110226650212,1.02586827095145))
REPRESENTATION_ITEM('')
);
#420=(
BOUNDED_CURVE()
B_SPLINE_CURVE(2,(#109509,#109510,#109511),.UNSPECIFIED.,.F.,.F.)
B_SPLINE_CURVE_WITH_KNOTS((3,3),(0.0254220173370218,0.0414764624875315),
 .UNSPECIFIED.)
CURVE()
GEOMETRIC_REPRESENTATION_ITEM()
RATIONAL_B_SPLINE_CURVE((1.02586827095069,1.02110226650151,1.))
REPRESENTATION_ITEM('')
);
#421=(
BOUNDED_CURVE()
B_SPLINE_CURVE(2,(#109513,#109514,#109515),.UNSPECIFIED.,.F.,.F.)
B_SPLINE_CURVE_WITH_KNOTS((3,3),(0.,0.0160544451505064),.UNSPECIFIED.)
CURVE()
GEOMETRIC_REPRESENTATION_ITEM()
RATIONAL_B_SPLINE_CURVE((1.,1.02110226650114,1.02586827095025))
REPRESENTATION_ITEM('')
);
#422=(
BOUNDED_CURVE()
B_SPLINE_CURVE(2,(#109519,#109520,#109521),.UNSPECIFIED.,.F.,.F.)
B_SPLINE_CURVE_WITH_KNOTS((3,3),(0.025422017337023,0.0414764624875296),
 .UNSPECIFIED.)
CURVE()
GEOMETRIC_REPRESENTATION_ITEM()
RATIONAL_B_SPLINE_CURVE((1.02586827095025,1.02110226650115,1.))
REPRESENTATION_ITEM('')
);
#423=(
BOUNDED_CURVE()
B_SPLINE_CURVE(2,(#109523,#109524,#109525),.UNSPECIFIED.,.F.,.F.)
B_SPLINE_CURVE_WITH_KNOTS((3,3),(0.,0.0160544451505046),.UNSPECIFIED.)
CURVE()
GEOMETRIC_REPRESENTATION_ITEM()
RATIONAL_B_SPLINE_CURVE((1.,1.0211022665016,1.02586827095081))
REPRESENTATION_ITEM('')
);
#424=(
BOUNDED_CURVE()
B_SPLINE_CURVE(2,(#109529,#109530,#109531),.UNSPECIFIED.,.F.,.F.)
B_SPLINE_CURVE_WITH_KNOTS((3,3),(0.0254220173370246,0.0414764624875251),
 .UNSPECIFIED.)
CURVE()
GEOMETRIC_REPRESENTATION_ITEM()
RATIONAL_B_SPLINE_CURVE((1.02586827095081,1.0211022665016,1.))
REPRESENTATION_ITEM('')
);
#425=(
BOUNDED_CURVE()
B_SPLINE_CURVE(2,(#109533,#109534,#109535),.UNSPECIFIED.,.F.,.F.)
B_SPLINE_CURVE_WITH_KNOTS((3,3),(0.,0.0160544451505003),.UNSPECIFIED.)
CURVE()
GEOMETRIC_REPRESENTATION_ITEM()
RATIONAL_B_SPLINE_CURVE((1.,1.02110226650136,1.02586827095051))
REPRESENTATION_ITEM('')
);
#426=(
BOUNDED_CURVE()
B_SPLINE_CURVE(2,(#109539,#109540,#109541),.UNSPECIFIED.,.F.,.F.)
B_SPLINE_CURVE_WITH_KNOTS((3,3),(0.0254220173370209,0.0414764624875271),
 .UNSPECIFIED.)
CURVE()
GEOMETRIC_REPRESENTATION_ITEM()
RATIONAL_B_SPLINE_CURVE((1.02586827094991,1.02110226650087,1.))
REPRESENTATION_ITEM('')
);
#427=(
BOUNDED_CURVE()
B_SPLINE_CURVE(2,(#109543,#109544,#109545),.UNSPECIFIED.,.F.,.F.)
B_SPLINE_CURVE_WITH_KNOTS((3,3),(0.,0.0160544451505053),.UNSPECIFIED.)
CURVE()
GEOMETRIC_REPRESENTATION_ITEM()
RATIONAL_B_SPLINE_CURVE((1.,1.02110226650082,1.02586827094985))
REPRESENTATION_ITEM('')
);
#428=(
BOUNDED_CURVE()
B_SPLINE_CURVE(2,(#109549,#109550,#109551),.UNSPECIFIED.,.F.,.F.)
B_SPLINE_CURVE_WITH_KNOTS((3,3),(0.0254220173370217,0.0414764624875263),
 .UNSPECIFIED.)
CURVE()
GEOMETRIC_REPRESENTATION_ITEM()
RATIONAL_B_SPLINE_CURVE((1.02586827094985,1.02110226650082,1.))
REPRESENTATION_ITEM('')
);
#429=(
BOUNDED_CURVE()
B_SPLINE_CURVE(2,(#109553,#109554,#109555),.UNSPECIFIED.,.F.,.F.)
B_SPLINE_CURVE_WITH_KNOTS((3,3),(0.,0.0160544451505048),.UNSPECIFIED.)
CURVE()
GEOMETRIC_REPRESENTATION_ITEM()
RATIONAL_B_SPLINE_CURVE((1.,1.02110226650102,1.02586827095009))
REPRESENTATION_ITEM('')
);
#430=(
BOUNDED_CURVE()
B_SPLINE_CURVE(2,(#109558,#109559,#109560),.UNSPECIFIED.,.F.,.F.)
B_SPLINE_CURVE_WITH_KNOTS((3,3),(0.0254220173370231,0.0414764624875254),
 .UNSPECIFIED.)
CURVE()
GEOMETRIC_REPRESENTATION_ITEM()
RATIONAL_B_SPLINE_CURVE((1.0258682709511,1.02110226650184,1.))
REPRESENTATION_ITEM('')
);
#529=SHAPE_REPRESENTATION_RELATIONSHIP('SRR','None',#114066,#547);
#547=ADVANCED_BREP_SHAPE_REPRESENTATION('',(#583),#113980);
#565=STYLED_ITEM('',(#114317),#583);
#583=MANIFOLD_SOLID_BREP(
'ISO 4026 - M3 x 4 - 45H (Bush Retaining Screw)',#60406);
#803=CYLINDRICAL_SURFACE('',#63345,0.96675);
#804=CYLINDRICAL_SURFACE('',#63347,0.96675);
#805=CYLINDRICAL_SURFACE('',#63348,0.96675);
#806=CYLINDRICAL_SURFACE('',#63349,0.96675);
#807=CYLINDRICAL_SURFACE('',#63350,0.96675);
#808=CYLINDRICAL_SURFACE('',#63351,0.96675);
#809=CYLINDRICAL_SURFACE('',#63352,0.739000000000001);
#810=CYLINDRICAL_SURFACE('',#63354,0.739000000000001);
#811=CYLINDRICAL_SURFACE('',#63356,0.739000000000001);
#812=CYLINDRICAL_SURFACE('',#63357,0.739000000000001);
#813=CYLINDRICAL_SURFACE('',#63358,0.739000000000001);
#814=CYLINDRICAL_SURFACE('',#63359,0.739000000000001);
#815=CYLINDRICAL_SURFACE('',#63367,0.739000000000001);
#816=CYLINDRICAL_SURFACE('',#63376,0.469615242270667);
#817=CYLINDRICAL_SURFACE('',#63378,0.469615242270667);
#818=CYLINDRICAL_SURFACE('',#63380,0.469615242270667);
#819=CYLINDRICAL_SURFACE('',#63382,0.469615242270667);
#820=CYLINDRICAL_SURFACE('',#63384,0.469615242270667);
#821=CYLINDRICAL_SURFACE('',#63386,0.469615242270667);
#822=CYLINDRICAL_SURFACE('',#63416,0.96675);
#945=CONICAL_SURFACE('',#63368,0.569615242270665,0.785398163397437);
#946=CONICAL_SURFACE('',#63409,0.519615242270657,1.02974425867665);
#947=CONICAL_SURFACE('',#63415,0.88000000000001,0.78539816339743);
#948=CONICAL_SURFACE('',#63418,0.749999999999993,0.785398163397435);
#1390=CIRCLE('',#63346,0.96675);
#1391=CIRCLE('',#63353,0.739000000000001);
#1392=CIRCLE('',#63355,0.739000000000001);
#1393=CIRCLE('',#63361,0.96675);
#1394=CIRCLE('',#63362,0.96675);
#1395=CIRCLE('',#63364,0.96675);
#1396=CIRCLE('',#63365,0.96675);
#1397=CIRCLE('',#63366,0.739000000000001);
#1398=CIRCLE('',#63369,0.669615242270665);
#1399=CIRCLE('',#63370,0.469615242270667);
#1400=CIRCLE('',#63371,0.469615242270667);
#1401=CIRCLE('',#63372,0.469615242270667);
#1402=CIRCLE('',#63373,0.469615242270667);
#1403=CIRCLE('',#63374,0.469615242270667);
#1404=CIRCLE('',#63375,0.469615242270667);
#1405=CIRCLE('',#63377,0.469615242270667);
#1406=CIRCLE('',#63379,0.469615242270667);
#1407=CIRCLE('',#63381,0.469615242270667);
#1408=CIRCLE('',#63383,0.469615242270667);
#1409=CIRCLE('',#63385,0.469615242270667);
#1410=CIRCLE('',#63387,0.469615242270667);
#1411=CIRCLE('',#63398,0.519615242270657);
#1412=CIRCLE('',#63400,0.519615242270657);
#1413=CIRCLE('',#63402,0.519615242270657);
#1414=CIRCLE('',#63404,0.519615242270657);
#1415=CIRCLE('',#63406,0.519615242270657);
#1416=CIRCLE('',#63408,0.519615242270657);
#1417=CIRCLE('',#63414,0.760000000000005);
#1418=CIRCLE('',#63417,0.96675);
#1419=CIRCLE('',#63419,0.500000000000007);
#1855=FACE_BOUND('',#10658,.T.);
#3859=PLANE('',#63360);
#3860=PLANE('',#63363);
#3861=PLANE('',#63388);
#3862=PLANE('',#63389);
#3863=PLANE('',#63390);
#3864=PLANE('',#63391);
#3865=PLANE('',#63392);
#3866=PLANE('',#63393);
#3867=PLANE('',#63394);
#3868=PLANE('',#63395);
#3869=PLANE('',#63396);
#3870=PLANE('',#63397);
#3871=PLANE('',#63399);
#3872=PLANE('',#63401);
#3873=PLANE('',#63403);
#3874=PLANE('',#63405);
#3875=PLANE('',#63407);
#3876=PLANE('',#63410);
#3877=PLANE('',#63411);
#3878=PLANE('',#63412);
#3879=PLANE('',#63413);
#3880=PLANE('',#63420);
#7034=FACE_OUTER_BOUND('',#10614,.T.);
#7035=FACE_OUTER_BOUND('',#10615,.T.);
#7036=FACE_OUTER_BOUND('',#10616,.T.);
#7037=FACE_OUTER_BOUND('',#10617,.T.);
#7038=FACE_OUTER_BOUND('',#10618,.T.);
#7039=FACE_OUTER_BOUND('',#10619,.T.);
#7040=FACE_OUTER_BOUND('',#10620,.T.);
#7041=FACE_OUTER_BOUND('',#10621,.T.);
#7042=FACE_OUTER_BOUND('',#10622,.T.);
#7043=FACE_OUTER_BOUND('',#10623,.T.);
#7044=FACE_OUTER_BOUND('',#10624,.T.);
#7045=FACE_OUTER_BOUND('',#10625,.T.);
#7046=FACE_OUTER_BOUND('',#10626,.T.);
#7047=FACE_OUTER_BOUND('',#10627,.T.);
#7048=FACE_OUTER_BOUND('',#10628,.T.);
#7049=FACE_OUTER_BOUND('',#10629,.T.);
#7050=FACE_OUTER_BOUND('',#10630,.T.);
#7051=FACE_OUTER_BOUND('',#10631,.T.);
#7052=FACE_OUTER_BOUND('',#10632,.T.);
#7053=FACE_OUTER_BOUND('',#10633,.T.);
#7054=FACE_OUTER_BOUND('',#10634,.T.);
#7055=FACE_OUTER_BOUND('',#10635,.T.);
#7056=FACE_OUTER_BOUND('',#10636,.T.);
#7057=FACE_OUTER_BOUND('',#10637,.T.);
#7058=FACE_OUTER_BOUND('',#10638,.T.);
#7059=FACE_OUTER_BOUND('',#10639,.T.);
#7060=FACE_OUTER_BOUND('',#10640,.T.);
#7061=FACE_OUTER_BOUND('',#10641,.T.);
#7062=FACE_OUTER_BOUND('',#10642,.T.);
#7063=FACE_OUTER_BOUND('',#10643,.T.);
#7064=FACE_OUTER_BOUND('',#10644,.T.);
#7065=FACE_OUTER_BOUND('',#10645,.T.);
#7066=FACE_OUTER_BOUND('',#10646,.T.);
#7067=FACE_OUTER_BOUND('',#10647,.T.);
#7068=FACE_OUTER_BOUND('',#10648,.T.);
#7069=FACE_OUTER_BOUND('',#10649,.T.);
#7070=FACE_OUTER_BOUND('',#10650,.T.);
#7071=FACE_OUTER_BOUND('',#10651,.T.);
#7072=FACE_OUTER_BOUND('',#10652,.T.);
#7073=FACE_OUTER_BOUND('',#10653,.T.);
#7074=FACE_OUTER_BOUND('',#10654,.T.);
#7075=FACE_OUTER_BOUND('',#10655,.T.);
#7076=FACE_OUTER_BOUND('',#10656,.T.);
#7077=FACE_OUTER_BOUND('',#10657,.T.);
#7078=FACE_OUTER_BOUND('',#10659,.T.);
#7079=FACE_OUTER_BOUND('',#10660,.T.);
#7080=FACE_OUTER_BOUND('',#10661,.T.);
#7081=FACE_OUTER_BOUND('',#10662,.T.);
#10614=EDGE_LOOP('',(#55017,#55018,#55019,#55020));
#10615=EDGE_LOOP('',(#55021,#55022,#55023,#55024));
#10616=EDGE_LOOP('',(#55025,#55026,#55027,#55028));
#10617=EDGE_LOOP('',(#55029,#55030,#55031,#55032));
#10618=EDGE_LOOP('',(#55033,#55034,#55035,#55036));
#10619=EDGE_LOOP('',(#55037,#55038,#55039,#55040));
#10620=EDGE_LOOP('',(#55041,#55042,#55043));
#10621=EDGE_LOOP('',(#55044,#55045,#55046,#55047,#55048));
#10622=EDGE_LOOP('',(#55049,#55050,#55051,#55052));
#10623=EDGE_LOOP('',(#55053,#55054,#55055,#55056));
#10624=EDGE_LOOP('',(#55057,#55058,#55059,#55060));
#10625=EDGE_LOOP('',(#55061,#55062,#55063,#55064));
#10626=EDGE_LOOP('',(#55065,#55066,#55067,#55068,#55069,#55070));
#10627=EDGE_LOOP('',(#55071,#55072,#55073,#55074,#55075,#55076,#55077,#55078,
#55079,#55080,#55081,#55082,#55083,#55084,#55085));
#10628=EDGE_LOOP('',(#55086,#55087,#55088,#55089,#55090));
#10629=EDGE_LOOP('',(#55091,#55092,#55093,#55094));
#10630=EDGE_LOOP('',(#55095,#55096,#55097,#55098,#55099,#55100,#55101,#55102,
#55103,#55104,#55105,#55106,#55107,#55108,#55109,#55110));
#10631=EDGE_LOOP('',(#55111,#55112,#55113,#55114,#55115,#55116,#55117,#55118,
#55119,#55120,#55121,#55122,#55123,#55124,#55125,#55126,#55127,#55128,#55129,
#55130,#55131));
#10632=EDGE_LOOP('',(#55132,#55133,#55134,#55135));
#10633=EDGE_LOOP('',(#55136,#55137,#55138,#55139));
#10634=EDGE_LOOP('',(#55140,#55141,#55142,#55143));
#10635=EDGE_LOOP('',(#55144,#55145,#55146,#55147));
#10636=EDGE_LOOP('',(#55148,#55149,#55150,#55151));
#10637=EDGE_LOOP('',(#55152,#55153,#55154,#55155));
#10638=EDGE_LOOP('',(#55156,#55157,#55158,#55159,#55160,#55161,#55162,#55163));
#10639=EDGE_LOOP('',(#55164,#55165,#55166,#55167,#55168,#55169,#55170,#55171));
#10640=EDGE_LOOP('',(#55172,#55173,#55174,#55175,#55176,#55177,#55178,#55179));
#10641=EDGE_LOOP('',(#55180,#55181));
#10642=EDGE_LOOP('',(#55182,#55183));
#10643=EDGE_LOOP('',(#55184,#55185));
#10644=EDGE_LOOP('',(#55186,#55187));
#10645=EDGE_LOOP('',(#55188,#55189));
#10646=EDGE_LOOP('',(#55190,#55191));
#10647=EDGE_LOOP('',(#55192,#55193));
#10648=EDGE_LOOP('',(#55194,#55195));
#10649=EDGE_LOOP('',(#55196,#55197));
#10650=EDGE_LOOP('',(#55198,#55199));
#10651=EDGE_LOOP('',(#55200,#55201));
#10652=EDGE_LOOP('',(#55202,#55203));
#10653=EDGE_LOOP('',(#55204,#55205,#55206,#55207,#55208,#55209,#55210,#55211));
#10654=EDGE_LOOP('',(#55212,#55213,#55214,#55215,#55216,#55217,#55218,#55219));
#10655=EDGE_LOOP('',(#55220,#55221,#55222,#55223,#55224,#55225,#55226,#55227));
#10656=EDGE_LOOP('',(#55228,#55229,#55230,#55231,#55232,#55233,#55234,#55235));
#10657=EDGE_LOOP('',(#55236));
#10658=EDGE_LOOP('',(#55237));
#10659=EDGE_LOOP('',(#55238,#55239,#55240,#55241,#55242,#55243));
#10660=EDGE_LOOP('',(#55244,#55245,#55246,#55247));
#10661=EDGE_LOOP('',(#55248,#55249,#55250,#55251,#55252,#55253));
#10662=EDGE_LOOP('',(#55254));
#16586=LINE('',#108401,#22620);
#16587=LINE('',#108425,#22621);
#16588=LINE('',#108473,#22622);
#16589=LINE('',#108521,#22623);
#16590=LINE('',#108575,#22624);
#16591=LINE('',#108623,#22625);
#16592=LINE('',#108671,#22626);
#16593=LINE('',#108682,#22627);
#16594=LINE('',#108708,#22628);
#16595=LINE('',#108732,#22629);
#16596=LINE('',#108757,#22630);
#16597=LINE('',#108782,#22631);
#16598=LINE('',#109501,#22632);
#16599=LINE('',#109563,#22633);
#16600=LINE('',#109565,#22634);
#16601=LINE('',#109569,#22635);
#16602=LINE('',#109571,#22636);
#16603=LINE('',#109575,#22637);
#16604=LINE('',#109578,#22638);
#16605=LINE('',#109581,#22639);
#16606=LINE('',#109583,#22640);
#16607=LINE('',#109587,#22641);
#16608=LINE('',#109590,#22642);
#16609=LINE('',#109593,#22643);
#16610=LINE('',#109596,#22644);
#16611=LINE('',#109598,#22645);
#16612=LINE('',#109600,#22646);
#16613=LINE('',#109602,#22647);
#16614=LINE('',#109603,#22648);
#16615=LINE('',#109605,#22649);
#16616=LINE('',#109607,#22650);
#16617=LINE('',#109608,#22651);
#16618=LINE('',#109610,#22652);
#16619=LINE('',#109612,#22653);
#16620=LINE('',#109613,#22654);
#16621=LINE('',#109617,#22655);
#16622=LINE('',#109620,#22656);
#16623=LINE('',#109622,#22657);
#16624=LINE('',#109625,#22658);
#16625=LINE('',#109635,#22659);
#16626=LINE('',#109638,#22660);
#16627=LINE('',#109642,#22661);
#16628=LINE('',#109644,#22662);
#16629=LINE('',#109646,#22663);
#16630=LINE('',#109652,#22664);
#16631=LINE('',#109658,#22665);
#22620=VECTOR('',#74960,0.999999999999996);
#22621=VECTOR('',#74965,0.999999999999996);
#22622=VECTOR('',#74968,0.999999999999996);
#22623=VECTOR('',#74971,0.999999999999996);
#22624=VECTOR('',#74974,0.999999999999996);
#22625=VECTOR('',#74977,0.999999999999996);
#22626=VECTOR('',#74980,0.739000000000001);
#22627=VECTOR('',#74985,0.739000000000001);
#22628=VECTOR('',#74990,0.739000000000001);
#22629=VECTOR('',#74993,0.739000000000001);
#22630=VECTOR('',#74996,0.739000000000001);
#22631=VECTOR('',#74999,0.739000000000001);
#22632=VECTOR('',#75020,0.569615242270665);
#22633=VECTOR('',#75035,10.);
#22634=VECTOR('',#75036,10.);
#22635=VECTOR('',#75041,10.);
#22636=VECTOR('',#75042,10.);
#22637=VECTOR('',#75047,10.);
#22638=VECTOR('',#75050,10.);
#22639=VECTOR('',#75053,10.);
#22640=VECTOR('',#75054,10.);
#22641=VECTOR('',#75059,10.);
#22642=VECTOR('',#75062,10.);
#22643=VECTOR('',#75065,10.);
#22644=VECTOR('',#75068,10.);
#22645=VECTOR('',#75071,10.);
#22646=VECTOR('',#75072,10.);
#22647=VECTOR('',#75073,10.);
#22648=VECTOR('',#75074,10.);
#22649=VECTOR('',#75077,10.);
#22650=VECTOR('',#75078,10.);
#22651=VECTOR('',#75079,10.);
#22652=VECTOR('',#75082,10.);
#22653=VECTOR('',#75083,10.);
#22654=VECTOR('',#75084,10.);
#22655=VECTOR('',#75091,10.);
#22656=VECTOR('',#75096,10.);
#22657=VECTOR('',#75099,10.);
#22658=VECTOR('',#75102,10.);
#22659=VECTOR('',#75119,10.);
#22660=VECTOR('',#75124,10.);
#22661=VECTOR('',#75129,0.519615242270657);
#22662=VECTOR('',#75132,10.);
#22663=VECTOR('',#75135,10.);
#22664=VECTOR('',#75144,0.88000000000001);
#22665=VECTOR('',#75153,0.749999999999993);
#24497=B_SPLINE_CURVE_WITH_KNOTS('',3,(#108403,#108404,#108405,#108406,
#108407,#108408,#108409,#108410,#108411,#108412),.UNSPECIFIED.,.F.,.F.,
(4,3,3,4),(-4.09157007060749,-3.96000416091332,-2.97000312068499,-2.06546402602184),
 .UNSPECIFIED.);
#24498=B_SPLINE_CURVE_WITH_KNOTS('',3,(#108415,#108416,#108417,#108418,
#108419,#108420,#108421),.UNSPECIFIED.,.F.,.F.,(4,3,4),(0.,0.990001040228323,
1.11548660900407),.UNSPECIFIED.);
#24499=B_SPLINE_CURVE_WITH_KNOTS('',3,(#108426,#108427,#108428,#108429,
#108430,#108431,#108432,#108433,#108434,#108435,#108436,#108437,#108438,
#108439,#108440,#108441,#108442,#108443,#108444,#108445,#108446,#108447),
 .UNSPECIFIED.,.F.,.F.,(4,3,3,3,3,3,3,4),(-10.3747553777871,-9.90001040228329,
-8.91000936205496,-7.92000832182663,-6.93000728159831,-5.94000624136997,
-4.95000520114165,-4.09157007060749),.UNSPECIFIED.);
#24500=B_SPLINE_CURVE_WITH_KNOTS('',3,(#108448,#108449,#108450,#108451,
#108452,#108453,#108454,#108455,#108456,#108457,#108458,#108459,#108460,
#108461,#108462,#108463,#108464,#108465,#108466,#108467,#108468,#108469),
 .UNSPECIFIED.,.F.,.F.,(4,3,3,3,3,3,3,4),(1.11548660900407,1.98000208045665,
2.97000312068498,3.96000416091331,4.95000520114164,5.94000624136997,6.9300072815983,
7.39867191618366),.UNSPECIFIED.);
#24501=B_SPLINE_CURVE_WITH_KNOTS('',3,(#108474,#108475,#108476,#108477,
#108478,#108479,#108480,#108481,#108482,#108483,#108484,#108485,#108486,
#108487,#108488,#108489,#108490,#108491,#108492,#108493,#108494,#108495),
 .UNSPECIFIED.,.F.,.F.,(4,3,3,3,3,3,3,4),(-16.6579406849667,-15.8400166436532,
-14.8500156034249,-13.8600145631966,-12.8700135229683,-11.8800124827399,
-10.8900114425116,-10.3747553777871),.UNSPECIFIED.);
#24502=B_SPLINE_CURVE_WITH_KNOTS('',3,(#108496,#108497,#108498,#108499,
#108500,#108501,#108502,#108503,#108504,#108505,#108506,#108507,#108508,
#108509,#108510,#108511,#108512,#108513,#108514,#108515,#108516,#108517),
 .UNSPECIFIED.,.F.,.F.,(4,3,3,3,3,3,3,4),(7.39867191618366,7.92000832182662,
8.91000936205495,9.90001040228327,10.8900114425116,11.8800124827399,12.8700135229683,
13.6818572233633),.UNSPECIFIED.);
#24503=B_SPLINE_CURVE_WITH_KNOTS('',3,(#108522,#108523,#108524,#108525,
#108526,#108527,#108528,#108529,#108530,#108531,#108532,#108533,#108534,
#108535,#108536,#108537,#108538,#108539,#108540,#108541,#108542,#108543,
#108544,#108545,#108546),.UNSPECIFIED.,.F.,.F.,(4,3,3,3,3,3,3,3,4),(-22.9411259921463,
-22.7700239252515,-21.7800228850232,-20.7900218447949,-19.8000208045666,
-18.8100197643382,-17.8200187241099,-16.8300176838816,-16.6579406849667),
 .UNSPECIFIED.);
#24504=B_SPLINE_CURVE_WITH_KNOTS('',3,(#108547,#108548,#108549,#108550,
#108551,#108552,#108553,#108554,#108555,#108556,#108557,#108558,#108559,
#108560,#108561,#108562,#108563,#108564,#108565,#108566,#108567,#108568,
#108569,#108570,#108571),.UNSPECIFIED.,.F.,.F.,(4,3,3,3,3,3,3,3,4),(13.6818572233633,
13.8600145631966,14.8500156034249,15.8400166436532,16.8300176838816,17.8200187241099,
18.8100197643382,19.8000208045666,19.9650425305428),.UNSPECIFIED.);
#24505=B_SPLINE_CURVE_WITH_KNOTS('',3,(#108576,#108577,#108578,#108579,
#108580,#108581,#108582,#108583,#108584,#108585,#108586,#108587,#108588,
#108589,#108590,#108591,#108592,#108593,#108594,#108595,#108596,#108597),
 .UNSPECIFIED.,.F.,.F.,(4,3,3,3,3,3,3,4),(-29.2243112993259,-28.7100301666215,
-27.7200291263932,-26.7300280861648,-25.7400270459365,-24.7500260057082,
-23.7600249654799,-22.9411259921463),.UNSPECIFIED.);
#24506=B_SPLINE_CURVE_WITH_KNOTS('',3,(#108598,#108599,#108600,#108601,
#108602,#108603,#108604,#108605,#108606,#108607,#108608,#108609,#108610,
#108611,#108612,#108613,#108614,#108615,#108616,#108617,#108618,#108619),
 .UNSPECIFIED.,.F.,.F.,(4,3,3,3,3,3,3,4),(19.9650425305428,20.7900218447949,
21.7800228850232,22.7700239252515,23.7600249654799,24.7500260057082,25.7400270459365,
26.2482278377224),.UNSPECIFIED.);
#24507=B_SPLINE_CURVE_WITH_KNOTS('',3,(#108624,#108625,#108626,#108627,
#108628,#108629,#108630,#108631,#108632,#108633,#108634,#108635,#108636,
#108637,#108638,#108639,#108640,#108641,#108642,#108643,#108644,#108645),
 .UNSPECIFIED.,.F.,.F.,(4,3,3,3,3,3,3,4),(-35.5074966065054,-34.6500364079915,
-33.6600353677631,-32.6700343275348,-31.6800332873065,-30.6900322470782,
-29.7000312068498,-29.2243112993259),.UNSPECIFIED.);
#24508=B_SPLINE_CURVE_WITH_KNOTS('',3,(#108646,#108647,#108648,#108649,
#108650,#108651,#108652,#108653,#108654,#108655,#108656,#108657,#108658,
#108659,#108660,#108661,#108662,#108663,#108664,#108665,#108666,#108667),
 .UNSPECIFIED.,.F.,.F.,(4,3,3,3,3,3,3,4),(26.2482278377224,26.7300280861648,
27.7200291263932,28.7100301666215,29.7000312068498,30.6900322470781,31.6800332873065,
32.531413144902),.UNSPECIFIED.);
#24509=B_SPLINE_CURVE_WITH_KNOTS('',3,(#108673,#108674,#108675,#108676,
#108677),.UNSPECIFIED.,.F.,.F.,(4,1,4),(47.1238898038469,47.2564306455613,
48.1609697402245),.UNSPECIFIED.);
#24510=B_SPLINE_CURVE_WITH_KNOTS('',3,(#108683,#108684,#108685,#108686,
#108687,#108688,#108689,#108690,#108691,#108692),.UNSPECIFIED.,.F.,.F.,
(4,1,1,1,1,1,1,4),(40.8407044966673,41.3164244041913,42.3064254444196,43.296426484648,
44.2864275248763,45.2764285651046,46.2664296053329,47.1238898038469),
 .UNSPECIFIED.);
#24511=B_SPLINE_CURVE_WITH_KNOTS('',3,(#108695,#108696,#108697,#108698,
#108699,#108700,#108701,#108702,#108703,#108704),.UNSPECIFIED.,.F.,.F.,
(4,1,1,1,1,1,1,4),(40.8407044966673,40.9793256793001,41.9693267195284,42.9593277597568,
43.9493287999851,44.9393298402134,45.9293308804417,46.9193319206701),
 .UNSPECIFIED.);
#24512=B_SPLINE_CURVE_WITH_KNOTS('',3,(#108709,#108710,#108711,#108712,
#108713,#108714,#108715,#108716,#108717,#108718),.UNSPECIFIED.,.F.,.F.,
(4,1,1,1,1,1,1,4),(34.5575191894877,35.3764181628213,36.3664192030497,37.356420243278,
38.3464212835063,39.3364223237347,40.326423363963,40.8407044966673),
 .UNSPECIFIED.);
#24513=B_SPLINE_CURVE_WITH_KNOTS('',3,(#108719,#108720,#108721,#108722,
#108723,#108724,#108725,#108726,#108727,#108728),.UNSPECIFIED.,.F.,.F.,
(4,1,1,1,1,1,1,4),(34.5575191894877,35.0393194379301,36.0293204781585,37.0193215183868,
38.0093225586151,38.9993235988434,39.9893246390718,40.8407044966673),
 .UNSPECIFIED.);
#24514=B_SPLINE_CURVE_WITH_KNOTS('',3,(#108733,#108734,#108735,#108736,
#108737,#108738,#108739,#108740,#108741,#108742,#108743),.UNSPECIFIED.,
 .F.,.F.,(4,1,1,1,1,1,1,1,4),(28.2743338823082,28.4464108812231,29.4364119214514,
30.4264129616797,31.416414001908,32.4064150421364,33.3964160823647,34.386417122593,
34.5575191894877),.UNSPECIFIED.);
#24515=B_SPLINE_CURVE_WITH_KNOTS('',3,(#108744,#108745,#108746,#108747,
#108748,#108749,#108750,#108751,#108752,#108753),.UNSPECIFIED.,.F.,.F.,
(4,1,1,1,1,1,1,4),(28.2743338823081,29.0993131965602,30.0893142367885,31.0793152770168,
32.0693163172452,33.0593173574735,34.0493183977018,34.5575191894877),
 .UNSPECIFIED.);
#24516=B_SPLINE_CURVE_WITH_KNOTS('',3,(#108758,#108759,#108760,#108761,
#108762,#108763,#108764,#108765,#108766,#108767),.UNSPECIFIED.,.F.,.F.,
(4,1,1,1,1,1,1,4),(21.9911485751286,22.5064046398531,23.4964056800814,24.4864067203097,
25.4764077605381,26.4664088007664,27.4564098409947,28.2743338823082),
 .UNSPECIFIED.);
#24517=B_SPLINE_CURVE_WITH_KNOTS('',3,(#108768,#108769,#108770,#108771,
#108772,#108773,#108774,#108775,#108776,#108777,#108778),.UNSPECIFIED.,
 .F.,.F.,(4,1,1,1,1,1,1,1,4),(21.9911485751286,22.1693059149619,23.1593069551902,
24.1493079954185,25.1393090356469,26.1293100758752,27.1193111161035,28.1093121563318,
28.2743338823081),.UNSPECIFIED.);
#24518=B_SPLINE_CURVE_WITH_KNOTS('',3,(#108783,#108784,#108785,#108786,
#108787,#108788,#108789,#108790,#108791,#108792),.UNSPECIFIED.,.F.,.F.,
(4,1,1,1,1,1,1,4),(15.707963267949,16.5663983984831,17.5563994387115,18.5464004789398,
19.5364015191681,20.5264025593964,21.5164035996248,21.9911485751286),
 .UNSPECIFIED.);
#24519=B_SPLINE_CURVE_WITH_KNOTS('',3,(#108793,#108794,#108795,#108796,
#108797,#108798,#108799,#108800,#108801,#108802),.UNSPECIFIED.,.F.,.F.,
(4,1,1,1,1,1,1,4),(15.707963267949,16.2292996735919,17.2193007138202,18.2093017540486,
19.1993027942769,20.1893038345052,21.1793048747336,21.9911485751286),
 .UNSPECIFIED.);
#24520=B_SPLINE_CURVE_WITH_KNOTS('',3,(#108805,#108806,#108807,#108808,
#108809,#108810,#108811,#108812,#108813,#108814,#108815,#108816,#108817,
#108818,#108819,#108820,#108821,#108822,#108823,#108824,#108825,#108826,
#108827,#108828,#108829,#108830,#108831,#108832,#108833,#108834,#108835,
#108836,#108837,#108838,#108839,#108840,#108841,#108842,#108843,#108844,
#108845,#108846,#108847,#108848,#108849,#108850,#108851,#108852,#108853,
#108854,#108855,#108856,#108857,#108858,#108859,#108860,#108861,#108862,
#108863,#108864,#108865,#108866,#108867,#108868,#108869,#108870,#108871,
#108872,#108873,#108874,#108875,#108876,#108877),.UNSPECIFIED.,.F.,.F.,
(4,3,3,3,3,3,3,3,3,3,3,3,3,3,3,3,3,3,3,3,3,3,3,3,4),(-0.178587760439576,
-0.172123484066144,-0.162029610797555,-0.158960076316314,-0.156277673116426,
-0.145500175528421,-0.137612438657249,-0.135052164839013,-0.123703644030005,
-0.112271443891481,-0.106158017111512,-0.103756352114049,-0.0913724979174295,
-0.0799509356777508,-0.0747329310245961,-0.0722089888096775,-0.0698495451559696,
-0.0578987267473855,-0.0456650852971465,-0.0398988500531476,-0.0369271031414654,
-0.034358735828395,-0.0216670048239294,-0.00906125808895899,0.),
 .UNSPECIFIED.);
#24521=B_SPLINE_CURVE_WITH_KNOTS('',3,(#108882,#108883,#108884,#108885,
#108886,#108887,#108888,#108889,#108890,#108891,#108892,#108893,#108894,
#108895,#108896,#108897,#108898,#108899,#108900,#108901,#108902,#108903,
#108904,#108905,#108906,#108907,#108908,#108909,#108910,#108911,#108912,
#108913,#108914,#108915,#108916,#108917,#108918,#108919,#108920,#108921,
#108922,#108923,#108924,#108925,#108926,#108927,#108928,#108929,#108930,
#108931,#108932,#108933,#108934,#108935,#108936,#108937,#108938,#108939,
#108940,#108941,#108942,#108943,#108944,#108945,#108946,#108947,#108948,
#108949,#108950,#108951,#108952,#108953,#108954,#108955,#108956,#108957),
 .UNSPECIFIED.,.F.,.F.,(4,3,3,3,3,3,3,3,3,3,3,3,3,3,3,3,3,3,3,3,3,3,3,3,
3,4),(-0.177567088092011,-0.169323782934868,-0.158089696666802,-0.153262207767463,
-0.149988677353406,-0.137528660299912,-0.130268964361215,-0.127199953384994,
-0.124659149705796,-0.112713138690929,-0.101044919579301,-0.0953407172754274,
-0.0930414661610526,-0.0906321687534946,-0.0794510927903374,-0.0687820057106859,
-0.063254327381541,-0.0606631966659519,-0.0584063594980229,-0.0472188556442702,
-0.0361621989269624,-0.0310713136030704,-0.027770944652939,-0.0171899085459505,
-0.0069942035205897,0.),.UNSPECIFIED.);
#24522=B_SPLINE_CURVE_WITH_KNOTS('',3,(#109126,#109127,#109128,#109129,
#109130,#109131,#109132,#109133,#109134,#109135,#109136,#109137,#109138,
#109139,#109140,#109141),.UNSPECIFIED.,.F.,.F.,(4,3,3,3,3,4),(32.531413144902,
32.6700343275348,33.6600353677631,34.6500364079915,35.6400374482198,36.5445765428829),
 .UNSPECIFIED.);
#24523=B_SPLINE_CURVE_WITH_KNOTS('',3,(#109143,#109144,#109145,#109146,
#109147,#109148,#109149,#109150,#109151,#109152,#109153,#109154,#109155,
#109156,#109157,#109158,#109159,#109160,#109161,#109162,#109163,#109164,
#109165,#109166,#109167,#109168,#109169,#109170,#109171,#109172,#109173,
#109174,#109175,#109176,#109177,#109178,#109179,#109180,#109181,#109182,
#109183,#109184,#109185,#109186,#109187,#109188,#109189,#109190,#109191,
#109192,#109193,#109194,#109195,#109196,#109197,#109198,#109199,#109200,
#109201,#109202,#109203,#109204,#109205,#109206,#109207,#109208,#109209,
#109210,#109211,#109212,#109213,#109214,#109215),.UNSPECIFIED.,.F.,.F.,
(4,3,3,3,3,3,3,3,3,3,3,3,3,3,3,3,3,3,3,3,3,3,3,3,4),(-0.17858776043949,
-0.172123484066062,-0.162029610797479,-0.158960078532571,-0.156277675821071,
-0.145500180136282,-0.137612447812564,-0.135052182725417,-0.123703662522982,
-0.112271461769566,-0.106158041900681,-0.103756358640701,-0.0913724979173968,
-0.0799509356777222,-0.0747329304622504,-0.0722089814481734,-0.0698495348147565,
-0.0578987173311656,-0.0456650770053533,-0.0398988390332298,-0.0369269838058204,
-0.0343587144614106,-0.0216669841604778,-0.00906123403203008,0.),
 .UNSPECIFIED.);
#24524=B_SPLINE_CURVE_WITH_KNOTS('',3,(#109216,#109217,#109218,#109219,
#109220,#109221,#109222,#109223,#109224),.UNSPECIFIED.,.F.,.F.,(4,1,1,1,
1,1,4),(10.3747553777871,11.2792944724503,12.2692955126786,13.2592965529069,
14.2492975931353,15.2392986333636,15.707963267949),.UNSPECIFIED.);
#24525=B_SPLINE_CURVE_WITH_KNOTS('',3,(#109230,#109231,#109232,#109233,
#109234,#109235,#109236,#109237,#109238,#109239,#109240,#109241,#109242,
#109243,#109244,#109245,#109246,#109247,#109248,#109249,#109250,#109251,
#109252,#109253,#109254,#109255,#109256,#109257,#109258,#109259,#109260,
#109261,#109262,#109263,#109264,#109265,#109266,#109267,#109268,#109269,
#109270,#109271,#109272,#109273,#109274,#109275,#109276,#109277,#109278,
#109279,#109280,#109281,#109282,#109283,#109284,#109285,#109286,#109287,
#109288,#109289,#109290,#109291,#109292,#109293,#109294,#109295,#109296,
#109297,#109298,#109299,#109300,#109301,#109302,#109303,#109304,#109305),
 .UNSPECIFIED.,.F.,.F.,(4,3,3,3,3,3,3,3,3,3,3,3,3,3,3,3,3,3,3,3,3,3,3,3,
3,4),(-0.177567088092203,-0.169323782935046,-0.158089696666967,-0.153262206421705,
-0.149988677397371,-0.137528659982041,-0.130268964083088,-0.127199950909321,
-0.124659148761581,-0.112713135669775,-0.101044912712987,-0.0953407090796688,
-0.0930414624834283,-0.0906321680944933,-0.0794510927904141,-0.0687820319799606,
-0.0632543486467741,-0.0606634285098871,-0.0584066697739641,-0.0472191669545651,
-0.0361625070709391,-0.0310717437638542,-0.0277708925982038,-0.0171898619043016,
-0.00699416415736055,0.),.UNSPECIFIED.);
#24526=B_SPLINE_CURVE_WITH_KNOTS('',3,(#109308,#109309,#109310,#109311,
#109312,#109313,#109314,#109315),.UNSPECIFIED.,.F.,.F.,(4,1,1,1,1,4),(11.6163931973415,
12.6063942375698,13.5963952777981,14.5863963180265,15.5763973582548,15.707963267949),
 .UNSPECIFIED.);
#24527=B_SPLINE_CURVE_WITH_KNOTS('',3,(#109484,#109485,#109486,#109487,
#109488,#109489,#109490,#109491,#109492,#109493,#109494,#109495,#109496),
 .UNSPECIFIED.,.F.,.F.,(4,3,3,3,4),(-38.6100405689048,-37.6200395286764,
-36.6300384884481,-35.6400374482198,-35.5074966065054),.UNSPECIFIED.);
#29900=VERTEX_POINT('',#108399);
#29901=VERTEX_POINT('',#108400);
#29902=VERTEX_POINT('',#108402);
#29903=VERTEX_POINT('',#108413);
#29904=VERTEX_POINT('',#108423);
#29905=VERTEX_POINT('',#108424);
#29906=VERTEX_POINT('',#108471);
#29907=VERTEX_POINT('',#108472);
#29908=VERTEX_POINT('',#108519);
#29909=VERTEX_POINT('',#108520);
#29910=VERTEX_POINT('',#108573);
#29911=VERTEX_POINT('',#108574);
#29912=VERTEX_POINT('',#108621);
#29913=VERTEX_POINT('',#108622);
#29914=VERTEX_POINT('',#108669);
#29915=VERTEX_POINT('',#108670);
#29916=VERTEX_POINT('',#108672);
#29917=VERTEX_POINT('',#108680);
#29918=VERTEX_POINT('',#108681);
#29919=VERTEX_POINT('',#108693);
#29920=VERTEX_POINT('',#108706);
#29921=VERTEX_POINT('',#108707);
#29922=VERTEX_POINT('',#108730);
#29923=VERTEX_POINT('',#108731);
#29924=VERTEX_POINT('',#108755);
#29925=VERTEX_POINT('',#108756);
#29926=VERTEX_POINT('',#108780);
#29927=VERTEX_POINT('',#108781);
#29928=VERTEX_POINT('',#108804);
#29929=VERTEX_POINT('',#108878);
#29930=VERTEX_POINT('',#108880);
#29931=VERTEX_POINT('',#109142);
#29932=VERTEX_POINT('',#109226);
#29933=VERTEX_POINT('',#109229);
#29934=VERTEX_POINT('',#109498);
#29935=VERTEX_POINT('',#109500);
#29936=VERTEX_POINT('',#109502);
#29937=VERTEX_POINT('',#109506);
#29938=VERTEX_POINT('',#109508);
#29939=VERTEX_POINT('',#109512);
#29940=VERTEX_POINT('',#109516);
#29941=VERTEX_POINT('',#109518);
#29942=VERTEX_POINT('',#109522);
#29943=VERTEX_POINT('',#109526);
#29944=VERTEX_POINT('',#109528);
#29945=VERTEX_POINT('',#109532);
#29946=VERTEX_POINT('',#109536);
#29947=VERTEX_POINT('',#109538);
#29948=VERTEX_POINT('',#109542);
#29949=VERTEX_POINT('',#109546);
#29950=VERTEX_POINT('',#109548);
#29951=VERTEX_POINT('',#109552);
#29952=VERTEX_POINT('',#109556);
#29953=VERTEX_POINT('',#109562);
#29954=VERTEX_POINT('',#109564);
#29955=VERTEX_POINT('',#109568);
#29956=VERTEX_POINT('',#109570);
#29957=VERTEX_POINT('',#109574);
#29958=VERTEX_POINT('',#109576);
#29959=VERTEX_POINT('',#109580);
#29960=VERTEX_POINT('',#109582);
#29961=VERTEX_POINT('',#109586);
#29962=VERTEX_POINT('',#109588);
#29963=VERTEX_POINT('',#109592);
#29964=VERTEX_POINT('',#109594);
#29965=VERTEX_POINT('',#109599);
#29966=VERTEX_POINT('',#109601);
#29967=VERTEX_POINT('',#109606);
#29968=VERTEX_POINT('',#109611);
#29969=VERTEX_POINT('',#109624);
#29970=VERTEX_POINT('',#109634);
#29971=VERTEX_POINT('',#109641);
#29972=VERTEX_POINT('',#109649);
#29973=VERTEX_POINT('',#109656);
#38341=EDGE_CURVE('',#29900,#29901,#16586,.T.);
#38342=EDGE_CURVE('',#29900,#29902,#24497,.T.);
#38343=EDGE_CURVE('',#29902,#29903,#1390,.T.);
#38344=EDGE_CURVE('',#29903,#29901,#24498,.T.);
#38345=EDGE_CURVE('',#29904,#29905,#16587,.T.);
#38346=EDGE_CURVE('',#29904,#29900,#24499,.T.);
#38347=EDGE_CURVE('',#29901,#29905,#24500,.T.);
#38348=EDGE_CURVE('',#29906,#29907,#16588,.T.);
#38349=EDGE_CURVE('',#29906,#29904,#24501,.T.);
#38350=EDGE_CURVE('',#29905,#29907,#24502,.T.);
#38351=EDGE_CURVE('',#29908,#29909,#16589,.T.);
#38352=EDGE_CURVE('',#29908,#29906,#24503,.T.);
#38353=EDGE_CURVE('',#29907,#29909,#24504,.T.);
#38354=EDGE_CURVE('',#29910,#29911,#16590,.T.);
#38355=EDGE_CURVE('',#29910,#29908,#24505,.T.);
#38356=EDGE_CURVE('',#29909,#29911,#24506,.T.);
#38357=EDGE_CURVE('',#29912,#29913,#16591,.T.);
#38358=EDGE_CURVE('',#29912,#29910,#24507,.T.);
#38359=EDGE_CURVE('',#29911,#29913,#24508,.T.);
#38360=EDGE_CURVE('',#29914,#29915,#16592,.T.);
#38361=EDGE_CURVE('',#29914,#29916,#24509,.T.);
#38362=EDGE_CURVE('',#29915,#29916,#1391,.T.);
#38363=EDGE_CURVE('',#29917,#29918,#16593,.T.);
#38364=EDGE_CURVE('',#29917,#29914,#24510,.T.);
#38365=EDGE_CURVE('',#29919,#29915,#1392,.T.);
#38366=EDGE_CURVE('',#29918,#29919,#24511,.T.);
#38367=EDGE_CURVE('',#29920,#29921,#16594,.T.);
#38368=EDGE_CURVE('',#29920,#29917,#24512,.T.);
#38369=EDGE_CURVE('',#29921,#29918,#24513,.T.);
#38370=EDGE_CURVE('',#29922,#29923,#16595,.T.);
#38371=EDGE_CURVE('',#29922,#29920,#24514,.T.);
#38372=EDGE_CURVE('',#29923,#29921,#24515,.T.);
#38373=EDGE_CURVE('',#29924,#29925,#16596,.T.);
#38374=EDGE_CURVE('',#29924,#29922,#24516,.T.);
#38375=EDGE_CURVE('',#29925,#29923,#24517,.T.);
#38376=EDGE_CURVE('',#29926,#29927,#16597,.T.);
#38377=EDGE_CURVE('',#29926,#29924,#24518,.T.);
#38378=EDGE_CURVE('',#29927,#29925,#24519,.T.);
#38379=EDGE_CURVE('',#29916,#29928,#24520,.T.);
#38380=EDGE_CURVE('',#29929,#29928,#1393,.F.);
#38381=EDGE_CURVE('',#29930,#29929,#1394,.F.);
#38382=EDGE_CURVE('',#29930,#29919,#24521,.T.);
#38383=EDGE_CURVE('',#29913,#29930,#24522,.T.);
#38384=EDGE_CURVE('',#29931,#29903,#24523,.T.);
#38385=EDGE_CURVE('',#29931,#29927,#24524,.T.);
#38386=EDGE_CURVE('',#29903,#29932,#1395,.T.);
#38387=EDGE_CURVE('',#29932,#29902,#1396,.T.);
#38388=EDGE_CURVE('',#29902,#29933,#24525,.T.);
#38389=EDGE_CURVE('',#29933,#29931,#1397,.T.);
#38390=EDGE_CURVE('',#29933,#29926,#24526,.T.);
#38391=EDGE_CURVE('',#29928,#29912,#24527,.T.);
#38392=EDGE_CURVE('',#29934,#29934,#1398,.T.);
#38393=EDGE_CURVE('',#29934,#29935,#16598,.T.);
#38394=EDGE_CURVE('',#29936,#29935,#419,.T.);
#38395=EDGE_CURVE('',#29936,#29937,#1399,.T.);
#38396=EDGE_CURVE('',#29938,#29937,#420,.T.);
#38397=EDGE_CURVE('',#29939,#29938,#421,.T.);
#38398=EDGE_CURVE('',#29939,#29940,#1400,.T.);
#38399=EDGE_CURVE('',#29941,#29940,#422,.T.);
#38400=EDGE_CURVE('',#29942,#29941,#423,.T.);
#38401=EDGE_CURVE('',#29942,#29943,#1401,.T.);
#38402=EDGE_CURVE('',#29944,#29943,#424,.T.);
#38403=EDGE_CURVE('',#29945,#29944,#425,.T.);
#38404=EDGE_CURVE('',#29945,#29946,#1402,.T.);
#38405=EDGE_CURVE('',#29947,#29946,#426,.T.);
#38406=EDGE_CURVE('',#29948,#29947,#427,.T.);
#38407=EDGE_CURVE('',#29948,#29949,#1403,.T.);
#38408=EDGE_CURVE('',#29950,#29949,#428,.T.);
#38409=EDGE_CURVE('',#29951,#29950,#429,.T.);
#38410=EDGE_CURVE('',#29951,#29952,#1404,.T.);
#38411=EDGE_CURVE('',#29935,#29952,#430,.T.);
#38412=EDGE_CURVE('',#29940,#29953,#16599,.T.);
#38413=EDGE_CURVE('',#29954,#29939,#16600,.T.);
#38414=EDGE_CURVE('',#29953,#29954,#1405,.T.);
#38415=EDGE_CURVE('',#29943,#29955,#16601,.T.);
#38416=EDGE_CURVE('',#29956,#29942,#16602,.T.);
#38417=EDGE_CURVE('',#29955,#29956,#1406,.T.);
#38418=EDGE_CURVE('',#29957,#29936,#16603,.T.);
#38419=EDGE_CURVE('',#29958,#29957,#1407,.T.);
#38420=EDGE_CURVE('',#29937,#29958,#16604,.T.);
#38421=EDGE_CURVE('',#29946,#29959,#16605,.T.);
#38422=EDGE_CURVE('',#29960,#29945,#16606,.T.);
#38423=EDGE_CURVE('',#29959,#29960,#1408,.T.);
#38424=EDGE_CURVE('',#29961,#29951,#16607,.T.);
#38425=EDGE_CURVE('',#29962,#29961,#1409,.T.);
#38426=EDGE_CURVE('',#29952,#29962,#16608,.T.);
#38427=EDGE_CURVE('',#29963,#29948,#16609,.T.);
#38428=EDGE_CURVE('',#29964,#29963,#1410,.T.);
#38429=EDGE_CURVE('',#29949,#29964,#16610,.T.);
#38430=EDGE_CURVE('',#29960,#29959,#16611,.T.);
#38431=EDGE_CURVE('',#29944,#29965,#16612,.T.);
#38432=EDGE_CURVE('',#29965,#29966,#16613,.T.);
#38433=EDGE_CURVE('',#29947,#29966,#16614,.T.);
#38434=EDGE_CURVE('',#29956,#29955,#16615,.T.);
#38435=EDGE_CURVE('',#29941,#29967,#16616,.T.);
#38436=EDGE_CURVE('',#29967,#29965,#16617,.T.);
#38437=EDGE_CURVE('',#29954,#29953,#16618,.T.);
#38438=EDGE_CURVE('',#29938,#29968,#16619,.T.);
#38439=EDGE_CURVE('',#29968,#29967,#16620,.T.);
#38440=EDGE_CURVE('',#29957,#29958,#16621,.T.);
#38441=EDGE_CURVE('',#29961,#29962,#16622,.T.);
#38442=EDGE_CURVE('',#29963,#29964,#16623,.T.);
#38443=EDGE_CURVE('',#29969,#29968,#16624,.T.);
#38444=EDGE_CURVE('',#29969,#29968,#1411,.T.);
#38445=EDGE_CURVE('',#29968,#29967,#1412,.T.);
#38446=EDGE_CURVE('',#29967,#29965,#1413,.T.);
#38447=EDGE_CURVE('',#29965,#29966,#1414,.T.);
#38448=EDGE_CURVE('',#29966,#29970,#16625,.T.);
#38449=EDGE_CURVE('',#29966,#29970,#1415,.T.);
#38450=EDGE_CURVE('',#29970,#29969,#16626,.T.);
#38451=EDGE_CURVE('',#29970,#29969,#1416,.T.);
#38452=EDGE_CURVE('',#29969,#29971,#16627,.T.);
#38453=EDGE_CURVE('',#29935,#29969,#16628,.T.);
#38454=EDGE_CURVE('',#29950,#29970,#16629,.T.);
#38455=EDGE_CURVE('',#29972,#29972,#1417,.T.);
#38456=EDGE_CURVE('',#29932,#29972,#16630,.T.);
#38457=EDGE_CURVE('',#29928,#29930,#1418,.F.);
#38458=EDGE_CURVE('',#29973,#29973,#1419,.T.);
#38459=EDGE_CURVE('',#29973,#29929,#16631,.T.);
#55017=ORIENTED_EDGE('',*,*,#38341,.F.);
#55018=ORIENTED_EDGE('',*,*,#38342,.T.);
#55019=ORIENTED_EDGE('',*,*,#38343,.T.);
#55020=ORIENTED_EDGE('',*,*,#38344,.T.);
#55021=ORIENTED_EDGE('',*,*,#38345,.F.);
#55022=ORIENTED_EDGE('',*,*,#38346,.T.);
#55023=ORIENTED_EDGE('',*,*,#38341,.T.);
#55024=ORIENTED_EDGE('',*,*,#38347,.T.);
#55025=ORIENTED_EDGE('',*,*,#38348,.F.);
#55026=ORIENTED_EDGE('',*,*,#38349,.T.);
#55027=ORIENTED_EDGE('',*,*,#38345,.T.);
#55028=ORIENTED_EDGE('',*,*,#38350,.T.);
#55029=ORIENTED_EDGE('',*,*,#38351,.F.);
#55030=ORIENTED_EDGE('',*,*,#38352,.T.);
#55031=ORIENTED_EDGE('',*,*,#38348,.T.);
#55032=ORIENTED_EDGE('',*,*,#38353,.T.);
#55033=ORIENTED_EDGE('',*,*,#38354,.F.);
#55034=ORIENTED_EDGE('',*,*,#38355,.T.);
#55035=ORIENTED_EDGE('',*,*,#38351,.T.);
#55036=ORIENTED_EDGE('',*,*,#38356,.T.);
#55037=ORIENTED_EDGE('',*,*,#38357,.F.);
#55038=ORIENTED_EDGE('',*,*,#38358,.T.);
#55039=ORIENTED_EDGE('',*,*,#38354,.T.);
#55040=ORIENTED_EDGE('',*,*,#38359,.T.);
#55041=ORIENTED_EDGE('',*,*,#38360,.F.);
#55042=ORIENTED_EDGE('',*,*,#38361,.T.);
#55043=ORIENTED_EDGE('',*,*,#38362,.F.);
#55044=ORIENTED_EDGE('',*,*,#38363,.F.);
#55045=ORIENTED_EDGE('',*,*,#38364,.T.);
#55046=ORIENTED_EDGE('',*,*,#38360,.T.);
#55047=ORIENTED_EDGE('',*,*,#38365,.F.);
#55048=ORIENTED_EDGE('',*,*,#38366,.F.);
#55049=ORIENTED_EDGE('',*,*,#38367,.F.);
#55050=ORIENTED_EDGE('',*,*,#38368,.T.);
#55051=ORIENTED_EDGE('',*,*,#38363,.T.);
#55052=ORIENTED_EDGE('',*,*,#38369,.F.);
#55053=ORIENTED_EDGE('',*,*,#38370,.F.);
#55054=ORIENTED_EDGE('',*,*,#38371,.T.);
#55055=ORIENTED_EDGE('',*,*,#38367,.T.);
#55056=ORIENTED_EDGE('',*,*,#38372,.F.);
#55057=ORIENTED_EDGE('',*,*,#38373,.F.);
#55058=ORIENTED_EDGE('',*,*,#38374,.T.);
#55059=ORIENTED_EDGE('',*,*,#38370,.T.);
#55060=ORIENTED_EDGE('',*,*,#38375,.F.);
#55061=ORIENTED_EDGE('',*,*,#38376,.F.);
#55062=ORIENTED_EDGE('',*,*,#38377,.T.);
#55063=ORIENTED_EDGE('',*,*,#38373,.T.);
#55064=ORIENTED_EDGE('',*,*,#38378,.F.);
#55065=ORIENTED_EDGE('',*,*,#38365,.T.);
#55066=ORIENTED_EDGE('',*,*,#38362,.T.);
#55067=ORIENTED_EDGE('',*,*,#38379,.T.);
#55068=ORIENTED_EDGE('',*,*,#38380,.F.);
#55069=ORIENTED_EDGE('',*,*,#38381,.F.);
#55070=ORIENTED_EDGE('',*,*,#38382,.T.);
#55071=ORIENTED_EDGE('',*,*,#38382,.F.);
#55072=ORIENTED_EDGE('',*,*,#38383,.F.);
#55073=ORIENTED_EDGE('',*,*,#38359,.F.);
#55074=ORIENTED_EDGE('',*,*,#38356,.F.);
#55075=ORIENTED_EDGE('',*,*,#38353,.F.);
#55076=ORIENTED_EDGE('',*,*,#38350,.F.);
#55077=ORIENTED_EDGE('',*,*,#38347,.F.);
#55078=ORIENTED_EDGE('',*,*,#38344,.F.);
#55079=ORIENTED_EDGE('',*,*,#38384,.F.);
#55080=ORIENTED_EDGE('',*,*,#38385,.T.);
#55081=ORIENTED_EDGE('',*,*,#38378,.T.);
#55082=ORIENTED_EDGE('',*,*,#38375,.T.);
#55083=ORIENTED_EDGE('',*,*,#38372,.T.);
#55084=ORIENTED_EDGE('',*,*,#38369,.T.);
#55085=ORIENTED_EDGE('',*,*,#38366,.T.);
#55086=ORIENTED_EDGE('',*,*,#38386,.T.);
#55087=ORIENTED_EDGE('',*,*,#38387,.T.);
#55088=ORIENTED_EDGE('',*,*,#38388,.T.);
#55089=ORIENTED_EDGE('',*,*,#38389,.T.);
#55090=ORIENTED_EDGE('',*,*,#38384,.T.);
#55091=ORIENTED_EDGE('',*,*,#38376,.T.);
#55092=ORIENTED_EDGE('',*,*,#38385,.F.);
#55093=ORIENTED_EDGE('',*,*,#38389,.F.);
#55094=ORIENTED_EDGE('',*,*,#38390,.T.);
#55095=ORIENTED_EDGE('',*,*,#38379,.F.);
#55096=ORIENTED_EDGE('',*,*,#38361,.F.);
#55097=ORIENTED_EDGE('',*,*,#38364,.F.);
#55098=ORIENTED_EDGE('',*,*,#38368,.F.);
#55099=ORIENTED_EDGE('',*,*,#38371,.F.);
#55100=ORIENTED_EDGE('',*,*,#38374,.F.);
#55101=ORIENTED_EDGE('',*,*,#38377,.F.);
#55102=ORIENTED_EDGE('',*,*,#38390,.F.);
#55103=ORIENTED_EDGE('',*,*,#38388,.F.);
#55104=ORIENTED_EDGE('',*,*,#38342,.F.);
#55105=ORIENTED_EDGE('',*,*,#38346,.F.);
#55106=ORIENTED_EDGE('',*,*,#38349,.F.);
#55107=ORIENTED_EDGE('',*,*,#38352,.F.);
#55108=ORIENTED_EDGE('',*,*,#38355,.F.);
#55109=ORIENTED_EDGE('',*,*,#38358,.F.);
#55110=ORIENTED_EDGE('',*,*,#38391,.F.);
#55111=ORIENTED_EDGE('',*,*,#38392,.F.);
#55112=ORIENTED_EDGE('',*,*,#38393,.T.);
#55113=ORIENTED_EDGE('',*,*,#38394,.F.);
#55114=ORIENTED_EDGE('',*,*,#38395,.T.);
#55115=ORIENTED_EDGE('',*,*,#38396,.F.);
#55116=ORIENTED_EDGE('',*,*,#38397,.F.);
#55117=ORIENTED_EDGE('',*,*,#38398,.T.);
#55118=ORIENTED_EDGE('',*,*,#38399,.F.);
#55119=ORIENTED_EDGE('',*,*,#38400,.F.);
#55120=ORIENTED_EDGE('',*,*,#38401,.T.);
#55121=ORIENTED_EDGE('',*,*,#38402,.F.);
#55122=ORIENTED_EDGE('',*,*,#38403,.F.);
#55123=ORIENTED_EDGE('',*,*,#38404,.T.);
#55124=ORIENTED_EDGE('',*,*,#38405,.F.);
#55125=ORIENTED_EDGE('',*,*,#38406,.F.);
#55126=ORIENTED_EDGE('',*,*,#38407,.T.);
#55127=ORIENTED_EDGE('',*,*,#38408,.F.);
#55128=ORIENTED_EDGE('',*,*,#38409,.F.);
#55129=ORIENTED_EDGE('',*,*,#38410,.T.);
#55130=ORIENTED_EDGE('',*,*,#38411,.F.);
#55131=ORIENTED_EDGE('',*,*,#38393,.F.);
#55132=ORIENTED_EDGE('',*,*,#38412,.F.);
#55133=ORIENTED_EDGE('',*,*,#38398,.F.);
#55134=ORIENTED_EDGE('',*,*,#38413,.F.);
#55135=ORIENTED_EDGE('',*,*,#38414,.F.);
#55136=ORIENTED_EDGE('',*,*,#38415,.F.);
#55137=ORIENTED_EDGE('',*,*,#38401,.F.);
#55138=ORIENTED_EDGE('',*,*,#38416,.F.);
#55139=ORIENTED_EDGE('',*,*,#38417,.F.);
#55140=ORIENTED_EDGE('',*,*,#38418,.F.);
#55141=ORIENTED_EDGE('',*,*,#38419,.F.);
#55142=ORIENTED_EDGE('',*,*,#38420,.F.);
#55143=ORIENTED_EDGE('',*,*,#38395,.F.);
#55144=ORIENTED_EDGE('',*,*,#38421,.F.);
#55145=ORIENTED_EDGE('',*,*,#38404,.F.);
#55146=ORIENTED_EDGE('',*,*,#38422,.F.);
#55147=ORIENTED_EDGE('',*,*,#38423,.F.);
#55148=ORIENTED_EDGE('',*,*,#38424,.F.);
#55149=ORIENTED_EDGE('',*,*,#38425,.F.);
#55150=ORIENTED_EDGE('',*,*,#38426,.F.);
#55151=ORIENTED_EDGE('',*,*,#38410,.F.);
#55152=ORIENTED_EDGE('',*,*,#38427,.F.);
#55153=ORIENTED_EDGE('',*,*,#38428,.F.);
#55154=ORIENTED_EDGE('',*,*,#38429,.F.);
#55155=ORIENTED_EDGE('',*,*,#38407,.F.);
#55156=ORIENTED_EDGE('',*,*,#38405,.T.);
#55157=ORIENTED_EDGE('',*,*,#38421,.T.);
#55158=ORIENTED_EDGE('',*,*,#38430,.F.);
#55159=ORIENTED_EDGE('',*,*,#38422,.T.);
#55160=ORIENTED_EDGE('',*,*,#38403,.T.);
#55161=ORIENTED_EDGE('',*,*,#38431,.T.);
#55162=ORIENTED_EDGE('',*,*,#38432,.T.);
#55163=ORIENTED_EDGE('',*,*,#38433,.F.);
#55164=ORIENTED_EDGE('',*,*,#38402,.T.);
#55165=ORIENTED_EDGE('',*,*,#38415,.T.);
#55166=ORIENTED_EDGE('',*,*,#38434,.F.);
#55167=ORIENTED_EDGE('',*,*,#38416,.T.);
#55168=ORIENTED_EDGE('',*,*,#38400,.T.);
#55169=ORIENTED_EDGE('',*,*,#38435,.T.);
#55170=ORIENTED_EDGE('',*,*,#38436,.T.);
#55171=ORIENTED_EDGE('',*,*,#38431,.F.);
#55172=ORIENTED_EDGE('',*,*,#38399,.T.);
#55173=ORIENTED_EDGE('',*,*,#38412,.T.);
#55174=ORIENTED_EDGE('',*,*,#38437,.F.);
#55175=ORIENTED_EDGE('',*,*,#38413,.T.);
#55176=ORIENTED_EDGE('',*,*,#38397,.T.);
#55177=ORIENTED_EDGE('',*,*,#38438,.T.);
#55178=ORIENTED_EDGE('',*,*,#38439,.T.);
#55179=ORIENTED_EDGE('',*,*,#38435,.F.);
#55180=ORIENTED_EDGE('',*,*,#38414,.T.);
#55181=ORIENTED_EDGE('',*,*,#38437,.T.);
#55182=ORIENTED_EDGE('',*,*,#38417,.T.);
#55183=ORIENTED_EDGE('',*,*,#38434,.T.);
#55184=ORIENTED_EDGE('',*,*,#38419,.T.);
#55185=ORIENTED_EDGE('',*,*,#38440,.T.);
#55186=ORIENTED_EDGE('',*,*,#38423,.T.);
#55187=ORIENTED_EDGE('',*,*,#38430,.T.);
#55188=ORIENTED_EDGE('',*,*,#38425,.T.);
#55189=ORIENTED_EDGE('',*,*,#38441,.T.);
#55190=ORIENTED_EDGE('',*,*,#38428,.T.);
#55191=ORIENTED_EDGE('',*,*,#38442,.T.);
#55192=ORIENTED_EDGE('',*,*,#38443,.F.);
#55193=ORIENTED_EDGE('',*,*,#38444,.T.);
#55194=ORIENTED_EDGE('',*,*,#38439,.F.);
#55195=ORIENTED_EDGE('',*,*,#38445,.T.);
#55196=ORIENTED_EDGE('',*,*,#38436,.F.);
#55197=ORIENTED_EDGE('',*,*,#38446,.T.);
#55198=ORIENTED_EDGE('',*,*,#38432,.F.);
#55199=ORIENTED_EDGE('',*,*,#38447,.T.);
#55200=ORIENTED_EDGE('',*,*,#38448,.F.);
#55201=ORIENTED_EDGE('',*,*,#38449,.T.);
#55202=ORIENTED_EDGE('',*,*,#38450,.F.);
#55203=ORIENTED_EDGE('',*,*,#38451,.T.);
#55204=ORIENTED_EDGE('',*,*,#38447,.F.);
#55205=ORIENTED_EDGE('',*,*,#38446,.F.);
#55206=ORIENTED_EDGE('',*,*,#38445,.F.);
#55207=ORIENTED_EDGE('',*,*,#38444,.F.);
#55208=ORIENTED_EDGE('',*,*,#38452,.T.);
#55209=ORIENTED_EDGE('',*,*,#38452,.F.);
#55210=ORIENTED_EDGE('',*,*,#38451,.F.);
#55211=ORIENTED_EDGE('',*,*,#38449,.F.);
#55212=ORIENTED_EDGE('',*,*,#38394,.T.);
#55213=ORIENTED_EDGE('',*,*,#38453,.T.);
#55214=ORIENTED_EDGE('',*,*,#38443,.T.);
#55215=ORIENTED_EDGE('',*,*,#38438,.F.);
#55216=ORIENTED_EDGE('',*,*,#38396,.T.);
#55217=ORIENTED_EDGE('',*,*,#38420,.T.);
#55218=ORIENTED_EDGE('',*,*,#38440,.F.);
#55219=ORIENTED_EDGE('',*,*,#38418,.T.);
#55220=ORIENTED_EDGE('',*,*,#38409,.T.);
#55221=ORIENTED_EDGE('',*,*,#38454,.T.);
#55222=ORIENTED_EDGE('',*,*,#38450,.T.);
#55223=ORIENTED_EDGE('',*,*,#38453,.F.);
#55224=ORIENTED_EDGE('',*,*,#38411,.T.);
#55225=ORIENTED_EDGE('',*,*,#38426,.T.);
#55226=ORIENTED_EDGE('',*,*,#38441,.F.);
#55227=ORIENTED_EDGE('',*,*,#38424,.T.);
#55228=ORIENTED_EDGE('',*,*,#38406,.T.);
#55229=ORIENTED_EDGE('',*,*,#38433,.T.);
#55230=ORIENTED_EDGE('',*,*,#38448,.T.);
#55231=ORIENTED_EDGE('',*,*,#38454,.F.);
#55232=ORIENTED_EDGE('',*,*,#38408,.T.);
#55233=ORIENTED_EDGE('',*,*,#38429,.T.);
#55234=ORIENTED_EDGE('',*,*,#38442,.F.);
#55235=ORIENTED_EDGE('',*,*,#38427,.T.);
#55236=ORIENTED_EDGE('',*,*,#38455,.F.);
#55237=ORIENTED_EDGE('',*,*,#38392,.T.);
#55238=ORIENTED_EDGE('',*,*,#38386,.F.);
#55239=ORIENTED_EDGE('',*,*,#38343,.F.);
#55240=ORIENTED_EDGE('',*,*,#38387,.F.);
#55241=ORIENTED_EDGE('',*,*,#38456,.T.);
#55242=ORIENTED_EDGE('',*,*,#38455,.T.);
#55243=ORIENTED_EDGE('',*,*,#38456,.F.);
#55244=ORIENTED_EDGE('',*,*,#38357,.T.);
#55245=ORIENTED_EDGE('',*,*,#38383,.T.);
#55246=ORIENTED_EDGE('',*,*,#38457,.F.);
#55247=ORIENTED_EDGE('',*,*,#38391,.T.);
#55248=ORIENTED_EDGE('',*,*,#38458,.F.);
#55249=ORIENTED_EDGE('',*,*,#38459,.T.);
#55250=ORIENTED_EDGE('',*,*,#38380,.T.);
#55251=ORIENTED_EDGE('',*,*,#38457,.T.);
#55252=ORIENTED_EDGE('',*,*,#38381,.T.);
#55253=ORIENTED_EDGE('',*,*,#38459,.F.);
#55254=ORIENTED_EDGE('',*,*,#38458,.T.);
#57119=B_SPLINE_SURFACE_WITH_KNOTS('',3,3,((#108958,#108959,#108960,#108961,
#108962,#108963,#108964,#108965,#108966,#108967,#108968,#108969,#108970,
#108971,#108972,#108973,#108974,#108975,#108976,#108977,#108978,#108979,
#108980,#108981,#108982,#108983,#108984,#108985,#108986,#108987,#108988,
#108989,#108990,#108991,#108992,#108993,#108994,#108995,#108996,#108997,
#108998,#108999),(#109000,#109001,#109002,#109003,#109004,#109005,#109006,
#109007,#109008,#109009,#109010,#109011,#109012,#109013,#109014,#109015,
#109016,#109017,#109018,#109019,#109020,#109021,#109022,#109023,#109024,
#109025,#109026,#109027,#109028,#109029,#109030,#109031,#109032,#109033,
#109034,#109035,#109036,#109037,#109038,#109039,#109040,#109041),(#109042,
#109043,#109044,#109045,#109046,#109047,#109048,#109049,#109050,#109051,
#109052,#109053,#109054,#109055,#109056,#109057,#109058,#109059,#109060,
#109061,#109062,#109063,#109064,#109065,#109066,#109067,#109068,#109069,
#109070,#109071,#109072,#109073,#109074,#109075,#109076,#109077,#109078,
#109079,#109080,#109081,#109082,#109083),(#109084,#109085,#109086,#109087,
#109088,#109089,#109090,#109091,#109092,#109093,#109094,#109095,#109096,
#109097,#109098,#109099,#109100,#109101,#109102,#109103,#109104,#109105,
#109106,#109107,#109108,#109109,#109110,#109111,#109112,#109113,#109114,
#109115,#109116,#109117,#109118,#109119,#109120,#109121,#109122,#109123,
#109124,#109125)),.UNSPECIFIED.,.F.,.F.,.F.,(4,4),(4,1,1,1,1,1,1,1,1,1,
1,1,1,1,1,1,1,1,1,1,1,1,1,1,1,1,1,1,1,1,1,1,1,1,1,1,1,1,1,4),(0.,0.026298304761587),
(8.3092913517653,9.29929239199363,10.289293432222,11.2792944724503,12.2692955126786,
13.2592965529069,14.2492975931353,15.2392986333636,16.2292996735919,17.2193007138202,
18.2093017540486,19.1993027942769,20.1893038345052,21.1793048747336,22.1693059149619,
23.1593069551902,24.1493079954185,25.1393090356469,26.1293100758752,27.1193111161035,
28.1093121563318,29.0993131965602,30.0893142367885,31.0793152770168,32.0693163172452,
33.0593173574735,34.0493183977018,35.0393194379301,36.0293204781585,37.0193215183868,
38.0093225586151,38.9993235988434,39.9893246390718,40.9793256793001,41.9693267195284,
42.9593277597568,43.9493287999851,44.9393298402134,45.9293308804417,46.9193319206701),
 .UNSPECIFIED.);
#57120=B_SPLINE_SURFACE_WITH_KNOTS('',3,3,((#109316,#109317,#109318,#109319,
#109320,#109321,#109322,#109323,#109324,#109325,#109326,#109327,#109328,
#109329,#109330,#109331,#109332,#109333,#109334,#109335,#109336,#109337,
#109338,#109339,#109340,#109341,#109342,#109343,#109344,#109345,#109346,
#109347,#109348,#109349,#109350,#109351,#109352,#109353,#109354,#109355,
#109356,#109357),(#109358,#109359,#109360,#109361,#109362,#109363,#109364,
#109365,#109366,#109367,#109368,#109369,#109370,#109371,#109372,#109373,
#109374,#109375,#109376,#109377,#109378,#109379,#109380,#109381,#109382,
#109383,#109384,#109385,#109386,#109387,#109388,#109389,#109390,#109391,
#109392,#109393,#109394,#109395,#109396,#109397,#109398,#109399),(#109400,
#109401,#109402,#109403,#109404,#109405,#109406,#109407,#109408,#109409,
#109410,#109411,#109412,#109413,#109414,#109415,#109416,#109417,#109418,
#109419,#109420,#109421,#109422,#109423,#109424,#109425,#109426,#109427,
#109428,#109429,#109430,#109431,#109432,#109433,#109434,#109435,#109436,
#109437,#109438,#109439,#109440,#109441),(#109442,#109443,#109444,#109445,
#109446,#109447,#109448,#109449,#109450,#109451,#109452,#109453,#109454,
#109455,#109456,#109457,#109458,#109459,#109460,#109461,#109462,#109463,
#109464,#109465,#109466,#109467,#109468,#109469,#109470,#109471,#109472,
#109473,#109474,#109475,#109476,#109477,#109478,#109479,#109480,#109481,
#109482,#109483)),.UNSPECIFIED.,.F.,.F.,.F.,(4,4),(4,1,1,1,1,1,1,1,1,1,
1,1,1,1,1,1,1,1,1,1,1,1,1,1,1,1,1,1,1,1,1,1,1,1,1,1,1,1,1,4),(0.,0.026298304761587),
(11.6163931973415,12.6063942375698,13.5963952777981,14.5863963180265,15.5763973582548,
16.5663983984831,17.5563994387115,18.5464004789398,19.5364015191681,20.5264025593964,
21.5164035996248,22.5064046398531,23.4964056800814,24.4864067203097,25.4764077605381,
26.4664088007664,27.4564098409947,28.4464108812231,29.4364119214514,30.4264129616797,
31.416414001908,32.4064150421364,33.3964160823647,34.386417122593,35.3764181628213,
36.3664192030497,37.356420243278,38.3464212835063,39.3364223237347,40.326423363963,
41.3164244041913,42.3064254444196,43.296426484648,44.2864275248763,45.2764285651046,
46.2664296053329,47.2564306455613,48.2464316857896,49.2364327260179,50.2264337662462),
 .UNSPECIFIED.);
#60134=ADVANCED_FACE('',(#7034),#803,.T.);
#60135=ADVANCED_FACE('',(#7035),#804,.T.);
#60136=ADVANCED_FACE('',(#7036),#805,.T.);
#60137=ADVANCED_FACE('',(#7037),#806,.T.);
#60138=ADVANCED_FACE('',(#7038),#807,.T.);
#60139=ADVANCED_FACE('',(#7039),#808,.T.);
#60140=ADVANCED_FACE('',(#7040),#809,.T.);
#60141=ADVANCED_FACE('',(#7041),#810,.T.);
#60142=ADVANCED_FACE('',(#7042),#811,.T.);
#60143=ADVANCED_FACE('',(#7043),#812,.T.);
#60144=ADVANCED_FACE('',(#7044),#813,.T.);
#60145=ADVANCED_FACE('',(#7045),#814,.T.);
#60146=ADVANCED_FACE('',(#7046),#3859,.T.);
#60147=ADVANCED_FACE('',(#7047),#57119,.F.);
#60148=ADVANCED_FACE('',(#7048),#3860,.F.);
#60149=ADVANCED_FACE('',(#7049),#815,.T.);
#60150=ADVANCED_FACE('',(#7050),#57120,.F.);
#60151=ADVANCED_FACE('',(#7051),#945,.F.);
#60152=ADVANCED_FACE('',(#7052),#816,.T.);
#60153=ADVANCED_FACE('',(#7053),#817,.T.);
#60154=ADVANCED_FACE('',(#7054),#818,.T.);
#60155=ADVANCED_FACE('',(#7055),#819,.T.);
#60156=ADVANCED_FACE('',(#7056),#820,.T.);
#60157=ADVANCED_FACE('',(#7057),#821,.T.);
#60158=ADVANCED_FACE('',(#7058),#3861,.F.);
#60159=ADVANCED_FACE('',(#7059),#3862,.F.);
#60160=ADVANCED_FACE('',(#7060),#3863,.F.);
#60161=ADVANCED_FACE('',(#7061),#3864,.T.);
#60162=ADVANCED_FACE('',(#7062),#3865,.T.);
#60163=ADVANCED_FACE('',(#7063),#3866,.T.);
#60164=ADVANCED_FACE('',(#7064),#3867,.T.);
#60165=ADVANCED_FACE('',(#7065),#3868,.T.);
#60166=ADVANCED_FACE('',(#7066),#3869,.T.);
#60167=ADVANCED_FACE('',(#7067),#3870,.F.);
#60168=ADVANCED_FACE('',(#7068),#3871,.F.);
#60169=ADVANCED_FACE('',(#7069),#3872,.F.);
#60170=ADVANCED_FACE('',(#7070),#3873,.F.);
#60171=ADVANCED_FACE('',(#7071),#3874,.F.);
#60172=ADVANCED_FACE('',(#7072),#3875,.F.);
#60173=ADVANCED_FACE('',(#7073),#946,.F.);
#60174=ADVANCED_FACE('',(#7074),#3876,.F.);
#60175=ADVANCED_FACE('',(#7075),#3877,.F.);
#60176=ADVANCED_FACE('',(#7076),#3878,.F.);
#60177=ADVANCED_FACE('',(#7077,#1855),#3879,.T.);
#60178=ADVANCED_FACE('',(#7078),#947,.T.);
#60179=ADVANCED_FACE('',(#7079),#822,.T.);
#60180=ADVANCED_FACE('',(#7080),#948,.T.);
#60181=ADVANCED_FACE('',(#7081),#3880,.T.);
#60406=CLOSED_SHELL('',(#60134,#60135,#60136,#60137,#60138,#60139,#60140,
#60141,#60142,#60143,#60144,#60145,#60146,#60147,#60148,#60149,#60150,#60151,
#60152,#60153,#60154,#60155,#60156,#60157,#60158,#60159,#60160,#60161,#60162,
#60163,#60164,#60165,#60166,#60167,#60168,#60169,#60170,#60171,#60172,#60173,
#60174,#60175,#60176,#60177,#60178,#60179,#60180,#60181));
#63344=AXIS2_PLACEMENT_3D('',#108397,#74956,#74957);
#63345=AXIS2_PLACEMENT_3D('',#108398,#74958,#74959);
#63346=AXIS2_PLACEMENT_3D('',#108414,#74961,#74962);
#63347=AXIS2_PLACEMENT_3D('',#108422,#74963,#74964);
#63348=AXIS2_PLACEMENT_3D('',#108470,#74966,#74967);
#63349=AXIS2_PLACEMENT_3D('',#108518,#74969,#74970);
#63350=AXIS2_PLACEMENT_3D('',#108572,#74972,#74973);
#63351=AXIS2_PLACEMENT_3D('',#108620,#74975,#74976);
#63352=AXIS2_PLACEMENT_3D('',#108668,#74978,#74979);
#63353=AXIS2_PLACEMENT_3D('',#108678,#74981,#74982);
#63354=AXIS2_PLACEMENT_3D('',#108679,#74983,#74984);
#63355=AXIS2_PLACEMENT_3D('',#108694,#74986,#74987);
#63356=AXIS2_PLACEMENT_3D('',#108705,#74988,#74989);
#63357=AXIS2_PLACEMENT_3D('',#108729,#74991,#74992);
#63358=AXIS2_PLACEMENT_3D('',#108754,#74994,#74995);
#63359=AXIS2_PLACEMENT_3D('',#108779,#74997,#74998);
#63360=AXIS2_PLACEMENT_3D('',#108803,#75000,#75001);
#63361=AXIS2_PLACEMENT_3D('',#108879,#75002,#75003);
#63362=AXIS2_PLACEMENT_3D('',#108881,#75004,#75005);
#63363=AXIS2_PLACEMENT_3D('',#109225,#75006,#75007);
#63364=AXIS2_PLACEMENT_3D('',#109227,#75008,#75009);
#63365=AXIS2_PLACEMENT_3D('',#109228,#75010,#75011);
#63366=AXIS2_PLACEMENT_3D('',#109306,#75012,#75013);
#63367=AXIS2_PLACEMENT_3D('',#109307,#75014,#75015);
#63368=AXIS2_PLACEMENT_3D('',#109497,#75016,#75017);
#63369=AXIS2_PLACEMENT_3D('',#109499,#75018,#75019);
#63370=AXIS2_PLACEMENT_3D('',#109507,#75021,#75022);
#63371=AXIS2_PLACEMENT_3D('',#109517,#75023,#75024);
#63372=AXIS2_PLACEMENT_3D('',#109527,#75025,#75026);
#63373=AXIS2_PLACEMENT_3D('',#109537,#75027,#75028);
#63374=AXIS2_PLACEMENT_3D('',#109547,#75029,#75030);
#63375=AXIS2_PLACEMENT_3D('',#109557,#75031,#75032);
#63376=AXIS2_PLACEMENT_3D('',#109561,#75033,#75034);
#63377=AXIS2_PLACEMENT_3D('',#109566,#75037,#75038);
#63378=AXIS2_PLACEMENT_3D('',#109567,#75039,#75040);
#63379=AXIS2_PLACEMENT_3D('',#109572,#75043,#75044);
#63380=AXIS2_PLACEMENT_3D('',#109573,#75045,#75046);
#63381=AXIS2_PLACEMENT_3D('',#109577,#75048,#75049);
#63382=AXIS2_PLACEMENT_3D('',#109579,#75051,#75052);
#63383=AXIS2_PLACEMENT_3D('',#109584,#75055,#75056);
#63384=AXIS2_PLACEMENT_3D('',#109585,#75057,#75058);
#63385=AXIS2_PLACEMENT_3D('',#109589,#75060,#75061);
#63386=AXIS2_PLACEMENT_3D('',#109591,#75063,#75064);
#63387=AXIS2_PLACEMENT_3D('',#109595,#75066,#75067);
#63388=AXIS2_PLACEMENT_3D('',#109597,#75069,#75070);
#63389=AXIS2_PLACEMENT_3D('',#109604,#75075,#75076);
#63390=AXIS2_PLACEMENT_3D('',#109609,#75080,#75081);
#63391=AXIS2_PLACEMENT_3D('',#109614,#75085,#75086);
#63392=AXIS2_PLACEMENT_3D('',#109615,#75087,#75088);
#63393=AXIS2_PLACEMENT_3D('',#109616,#75089,#75090);
#63394=AXIS2_PLACEMENT_3D('',#109618,#75092,#75093);
#63395=AXIS2_PLACEMENT_3D('',#109619,#75094,#75095);
#63396=AXIS2_PLACEMENT_3D('',#109621,#75097,#75098);
#63397=AXIS2_PLACEMENT_3D('',#109623,#75100,#75101);
#63398=AXIS2_PLACEMENT_3D('',#109626,#75103,#75104);
#63399=AXIS2_PLACEMENT_3D('',#109627,#75105,#75106);
#63400=AXIS2_PLACEMENT_3D('',#109628,#75107,#75108);
#63401=AXIS2_PLACEMENT_3D('',#109629,#75109,#75110);
#63402=AXIS2_PLACEMENT_3D('',#109630,#75111,#75112);
#63403=AXIS2_PLACEMENT_3D('',#109631,#75113,#75114);
#63404=AXIS2_PLACEMENT_3D('',#109632,#75115,#75116);
#63405=AXIS2_PLACEMENT_3D('',#109633,#75117,#75118);
#63406=AXIS2_PLACEMENT_3D('',#109636,#75120,#75121);
#63407=AXIS2_PLACEMENT_3D('',#109637,#75122,#75123);
#63408=AXIS2_PLACEMENT_3D('',#109639,#75125,#75126);
#63409=AXIS2_PLACEMENT_3D('',#109640,#75127,#75128);
#63410=AXIS2_PLACEMENT_3D('',#109643,#75130,#75131);
#63411=AXIS2_PLACEMENT_3D('',#109645,#75133,#75134);
#63412=AXIS2_PLACEMENT_3D('',#109647,#75136,#75137);
#63413=AXIS2_PLACEMENT_3D('',#109648,#75138,#75139);
#63414=AXIS2_PLACEMENT_3D('',#109650,#75140,#75141);
#63415=AXIS2_PLACEMENT_3D('',#109651,#75142,#75143);
#63416=AXIS2_PLACEMENT_3D('',#109653,#75145,#75146);
#63417=AXIS2_PLACEMENT_3D('',#109654,#75147,#75148);
#63418=AXIS2_PLACEMENT_3D('',#109655,#75149,#75150);
#63419=AXIS2_PLACEMENT_3D('',#109657,#75151,#75152);
#63420=AXIS2_PLACEMENT_3D('',#109659,#75154,#75155);
#74956=DIRECTION('axis',(0.,0.,1.));
#74957=DIRECTION('refdir',(1.,0.,0.));
#74958=DIRECTION('center_axis',(0.,-1.,0.));
#74959=DIRECTION('ref_axis',(1.,0.,0.));
#74960=DIRECTION('',(0.,1.,0.));
#74961=DIRECTION('center_axis',(0.,-1.,0.));
#74962=DIRECTION('ref_axis',(1.,0.,0.));
#74963=DIRECTION('center_axis',(0.,-1.,0.));
#74964=DIRECTION('ref_axis',(1.,0.,0.));
#74965=DIRECTION('',(0.,1.,0.));
#74966=DIRECTION('center_axis',(0.,-1.,0.));
#74967=DIRECTION('ref_axis',(1.,0.,0.));
#74968=DIRECTION('',(0.,1.,0.));
#74969=DIRECTION('center_axis',(0.,-1.,0.));
#74970=DIRECTION('ref_axis',(1.,0.,0.));
#74971=DIRECTION('',(0.,1.,0.));
#74972=DIRECTION('center_axis',(0.,-1.,0.));
#74973=DIRECTION('ref_axis',(1.,0.,0.));
#74974=DIRECTION('',(0.,1.,0.));
#74975=DIRECTION('center_axis',(0.,-1.,0.));
#74976=DIRECTION('ref_axis',(1.,0.,0.));
#74977=DIRECTION('',(0.,1.,0.));
#74978=DIRECTION('center_axis',(0.,-1.,0.));
#74979=DIRECTION('ref_axis',(1.,0.,1.20186524993251E-14));
#74980=DIRECTION('',(0.,-1.,0.));
#74981=DIRECTION('center_axis',(0.,-1.,0.));
#74982=DIRECTION('ref_axis',(1.,0.,1.20186524993251E-14));
#74983=DIRECTION('center_axis',(0.,-1.,0.));
#74984=DIRECTION('ref_axis',(1.,0.,1.20186524993251E-14));
#74985=DIRECTION('',(0.,-1.,0.));
#74986=DIRECTION('center_axis',(0.,-1.,0.));
#74987=DIRECTION('ref_axis',(1.,0.,1.20186524993251E-14));
#74988=DIRECTION('center_axis',(0.,-1.,0.));
#74989=DIRECTION('ref_axis',(1.,0.,1.20186524993251E-14));
#74990=DIRECTION('',(0.,-1.,0.));
#74991=DIRECTION('center_axis',(0.,-1.,0.));
#74992=DIRECTION('ref_axis',(1.,0.,1.20186524993251E-14));
#74993=DIRECTION('',(0.,-1.,0.));
#74994=DIRECTION('center_axis',(0.,-1.,0.));
#74995=DIRECTION('ref_axis',(1.,0.,1.20186524993251E-14));
#74996=DIRECTION('',(0.,-1.,0.));
#74997=DIRECTION('center_axis',(0.,-1.,0.));
#74998=DIRECTION('ref_axis',(1.,0.,1.20186524993251E-14));
#74999=DIRECTION('',(0.,-1.,0.));
#75000=DIRECTION('center_axis',(0.,1.,0.));
#75001=DIRECTION('ref_axis',(0.,0.,1.));
#75002=DIRECTION('center_axis',(0.,1.,0.));
#75003=DIRECTION('ref_axis',(1.,0.,0.));
#75004=DIRECTION('center_axis',(0.,1.,0.));
#75005=DIRECTION('ref_axis',(1.,0.,0.));
#75006=DIRECTION('center_axis',(0.,1.,0.));
#75007=DIRECTION('ref_axis',(0.,0.,1.));
#75008=DIRECTION('center_axis',(0.,-1.,0.));
#75009=DIRECTION('ref_axis',(1.,0.,0.));
#75010=DIRECTION('center_axis',(0.,-1.,0.));
#75011=DIRECTION('ref_axis',(1.,0.,0.));
#75012=DIRECTION('center_axis',(0.,1.,0.));
#75013=DIRECTION('ref_axis',(1.,0.,1.20186524993251E-14));
#75014=DIRECTION('center_axis',(0.,-1.,0.));
#75015=DIRECTION('ref_axis',(1.,0.,1.20186524993251E-14));
#75016=DIRECTION('center_axis',(0.,1.,0.));
#75017=DIRECTION('ref_axis',(1.,0.,0.));
#75018=DIRECTION('center_axis',(0.,-1.,0.));
#75019=DIRECTION('ref_axis',(1.,0.,0.));
#75020=DIRECTION('',(0.70710678118654,-0.707106781186555,8.65956056235484E-17));
#75021=DIRECTION('center_axis',(0.,-1.,0.));
#75022=DIRECTION('ref_axis',(1.,0.,0.));
#75023=DIRECTION('center_axis',(0.,-1.,0.));
#75024=DIRECTION('ref_axis',(1.,0.,0.));
#75025=DIRECTION('center_axis',(0.,-1.,0.));
#75026=DIRECTION('ref_axis',(1.,0.,0.));
#75027=DIRECTION('center_axis',(0.,-1.,0.));
#75028=DIRECTION('ref_axis',(1.,0.,0.));
#75029=DIRECTION('center_axis',(0.,-1.,0.));
#75030=DIRECTION('ref_axis',(1.,0.,0.));
#75031=DIRECTION('center_axis',(0.,-1.,0.));
#75032=DIRECTION('ref_axis',(1.,0.,0.));
#75033=DIRECTION('center_axis',(0.,-1.,0.));
#75034=DIRECTION('ref_axis',(1.,0.,0.));
#75035=DIRECTION('',(0.,1.,0.));
#75036=DIRECTION('',(0.,-1.,0.));
#75037=DIRECTION('center_axis',(0.,1.,0.));
#75038=DIRECTION('ref_axis',(1.,0.,0.));
#75039=DIRECTION('center_axis',(0.,-1.,0.));
#75040=DIRECTION('ref_axis',(1.,0.,0.));
#75041=DIRECTION('',(0.,1.,0.));
#75042=DIRECTION('',(0.,-1.,0.));
#75043=DIRECTION('center_axis',(0.,1.,0.));
#75044=DIRECTION('ref_axis',(1.,0.,0.));
#75045=DIRECTION('center_axis',(0.,-1.,0.));
#75046=DIRECTION('ref_axis',(1.,0.,0.));
#75047=DIRECTION('',(0.,-1.,0.));
#75048=DIRECTION('center_axis',(0.,1.,0.));
#75049=DIRECTION('ref_axis',(1.,0.,0.));
#75050=DIRECTION('',(0.,1.,0.));
#75051=DIRECTION('center_axis',(0.,-1.,0.));
#75052=DIRECTION('ref_axis',(1.,0.,0.));
#75053=DIRECTION('',(0.,1.,0.));
#75054=DIRECTION('',(0.,-1.,0.));
#75055=DIRECTION('center_axis',(0.,1.,0.));
#75056=DIRECTION('ref_axis',(1.,0.,0.));
#75057=DIRECTION('center_axis',(0.,-1.,0.));
#75058=DIRECTION('ref_axis',(1.,0.,0.));
#75059=DIRECTION('',(0.,-1.,0.));
#75060=DIRECTION('center_axis',(0.,1.,0.));
#75061=DIRECTION('ref_axis',(1.,0.,0.));
#75062=DIRECTION('',(0.,1.,0.));
#75063=DIRECTION('center_axis',(0.,-1.,0.));
#75064=DIRECTION('ref_axis',(1.,0.,0.));
#75065=DIRECTION('',(0.,-1.,0.));
#75066=DIRECTION('center_axis',(0.,1.,0.));
#75067=DIRECTION('ref_axis',(1.,0.,0.));
#75068=DIRECTION('',(0.,1.,0.));
#75069=DIRECTION('center_axis',(0.866025403784448,0.,0.499999999999983));
#75070=DIRECTION('ref_axis',(-0.499999999999983,0.,0.866025403784448));
#75071=DIRECTION('',(-0.499999999999983,0.,0.866025403784448));
#75072=DIRECTION('',(0.,-1.,0.));
#75073=DIRECTION('',(-0.499999999999983,0.,0.866025403784448));
#75074=DIRECTION('',(0.,-1.,0.));
#75075=DIRECTION('center_axis',(0.866025403784453,0.,-0.499999999999976));
#75076=DIRECTION('ref_axis',(0.499999999999976,0.,0.866025403784453));
#75077=DIRECTION('',(0.499999999999976,0.,0.866025403784453));
#75078=DIRECTION('',(0.,-1.,0.));
#75079=DIRECTION('',(0.499999999999976,0.,0.866025403784453));
#75080=DIRECTION('center_axis',(0.,0.,-1.));
#75081=DIRECTION('ref_axis',(1.,0.,0.));
#75082=DIRECTION('',(1.,0.,0.));
#75083=DIRECTION('',(0.,-1.,0.));
#75084=DIRECTION('',(1.,0.,0.));
#75085=DIRECTION('center_axis',(0.,1.,0.));
#75086=DIRECTION('ref_axis',(0.,0.,1.));
#75087=DIRECTION('center_axis',(0.,1.,0.));
#75088=DIRECTION('ref_axis',(0.,0.,1.));
#75089=DIRECTION('center_axis',(0.,1.,0.));
#75090=DIRECTION('ref_axis',(0.,0.,1.));
#75091=DIRECTION('',(0.499999999999976,0.,-0.866025403784453));
#75092=DIRECTION('center_axis',(0.,1.,0.));
#75093=DIRECTION('ref_axis',(0.,0.,1.));
#75094=DIRECTION('center_axis',(0.,1.,0.));
#75095=DIRECTION('ref_axis',(0.,0.,1.));
#75096=DIRECTION('',(-0.499999999999983,0.,-0.866025403784448));
#75097=DIRECTION('center_axis',(0.,1.,0.));
#75098=DIRECTION('ref_axis',(0.,0.,1.));
#75099=DIRECTION('',(-1.,0.,0.));
#75100=DIRECTION('center_axis',(0.,1.,0.));
#75101=DIRECTION('ref_axis',(0.,0.,1.));
#75102=DIRECTION('',(0.499999999999976,0.,-0.866025403784453));
#75103=DIRECTION('center_axis',(0.,-1.,0.));
#75104=DIRECTION('ref_axis',(1.,0.,0.));
#75105=DIRECTION('center_axis',(0.,1.,0.));
#75106=DIRECTION('ref_axis',(0.,0.,1.));
#75107=DIRECTION('center_axis',(0.,-1.,0.));
#75108=DIRECTION('ref_axis',(1.,0.,0.));
#75109=DIRECTION('center_axis',(0.,1.,0.));
#75110=DIRECTION('ref_axis',(0.,0.,1.));
#75111=DIRECTION('center_axis',(0.,-1.,0.));
#75112=DIRECTION('ref_axis',(1.,0.,0.));
#75113=DIRECTION('center_axis',(0.,1.,0.));
#75114=DIRECTION('ref_axis',(0.,0.,1.));
#75115=DIRECTION('center_axis',(0.,-1.,0.));
#75116=DIRECTION('ref_axis',(1.,0.,0.));
#75117=DIRECTION('center_axis',(0.,1.,0.));
#75118=DIRECTION('ref_axis',(0.,0.,1.));
#75119=DIRECTION('',(-1.,0.,0.));
#75120=DIRECTION('center_axis',(0.,-1.,0.));
#75121=DIRECTION('ref_axis',(1.,0.,0.));
#75122=DIRECTION('center_axis',(0.,1.,0.));
#75123=DIRECTION('ref_axis',(0.,0.,1.));
#75124=DIRECTION('',(-0.499999999999983,0.,-0.866025403784448));
#75125=DIRECTION('center_axis',(0.,-1.,0.));
#75126=DIRECTION('ref_axis',(1.,0.,0.));
#75127=DIRECTION('center_axis',(0.,1.,0.));
#75128=DIRECTION('ref_axis',(1.,0.,0.));
#75129=DIRECTION('',(0.857167300702109,-0.51503807491006,1.04972719113861E-16));
#75130=DIRECTION('center_axis',(-0.866025403784453,0.,-0.499999999999976));
#75131=DIRECTION('ref_axis',(0.499999999999976,0.,-0.866025403784453));
#75132=DIRECTION('',(0.,-1.,0.));
#75133=DIRECTION('center_axis',(-0.866025403784448,0.,0.499999999999983));
#75134=DIRECTION('ref_axis',(-0.499999999999983,0.,-0.866025403784448));
#75135=DIRECTION('',(0.,-1.,0.));
#75136=DIRECTION('center_axis',(0.,0.,1.));
#75137=DIRECTION('ref_axis',(-1.,0.,0.));
#75138=DIRECTION('center_axis',(0.,1.,0.));
#75139=DIRECTION('ref_axis',(0.,0.,1.));
#75140=DIRECTION('center_axis',(0.,-1.,0.));
#75141=DIRECTION('ref_axis',(1.,0.,0.));
#75142=DIRECTION('center_axis',(0.,-1.,0.));
#75143=DIRECTION('ref_axis',(1.,0.,0.));
#75144=DIRECTION('',(0.707106781186534,0.707106781186561,8.65956056235477E-17));
#75145=DIRECTION('center_axis',(0.,-1.,0.));
#75146=DIRECTION('ref_axis',(1.,0.,0.));
#75147=DIRECTION('center_axis',(0.,1.,0.));
#75148=DIRECTION('ref_axis',(1.,0.,0.));
#75149=DIRECTION('center_axis',(0.,1.,0.));
#75150=DIRECTION('ref_axis',(1.,0.,0.));
#75151=DIRECTION('center_axis',(0.,-1.,0.));
#75152=DIRECTION('ref_axis',(1.,0.,0.));
#75153=DIRECTION('',(-0.707106781186538,0.707106781186557,-8.65956056235482E-17));
#75154=DIRECTION('center_axis',(0.,-1.,0.));
#75155=DIRECTION('ref_axis',(0.,0.,-1.));
#108397=CARTESIAN_POINT('',(0.,0.,0.));
#108398=CARTESIAN_POINT('Origin',(110.,24.53,42.));
#108399=CARTESIAN_POINT('',(109.032306318989,25.5642640831103,42.0006908675261));
#108400=CARTESIAN_POINT('',(109.032548003746,25.6222359168897,42.0006735849849));
#108401=CARTESIAN_POINT('',(109.03325,24.53,42.));
#108402=CARTESIAN_POINT('',(110.425646355462,25.69325,42.8688267550426));
#108403=CARTESIAN_POINT('Ctrl Pts',(109.032306318989,25.5642640831103,42.0006908675261));
#108404=CARTESIAN_POINT('Ctrl Pts',(109.031974852187,25.5670559984264,42.0429741926217));
#108405=CARTESIAN_POINT('Ctrl Pts',(109.034508923572,25.5698479137424,42.0852164196326));
#108406=CARTESIAN_POINT('Ctrl Pts',(109.040044285781,25.5726398290584,42.1270598791021));
#108407=CARTESIAN_POINT('Ctrl Pts',(109.081696521971,25.5936483036209,42.4419215974445));
#108408=CARTESIAN_POINT('Ctrl Pts',(109.293287593117,25.6146567781833,42.7342043338243));
#108409=CARTESIAN_POINT('Ctrl Pts',(109.579443943085,25.6356652527458,42.8722111754205));
#108410=CARTESIAN_POINT('Ctrl Pts',(109.84089781557,25.6548601684972,42.9983045616719));
#108411=CARTESIAN_POINT('Ctrl Pts',(110.164598917808,25.6740550842486,42.9956081516571));
#108412=CARTESIAN_POINT('Ctrl Pts',(110.426173582409,25.69325,42.8693912864047));
#108413=CARTESIAN_POINT('',(109.574880871485,25.69325,42.8682622236805));
#108414=CARTESIAN_POINT('Origin',(110.,25.69325,42.));
#108415=CARTESIAN_POINT('Ctrl Pts',(109.574880871485,25.69325,42.8682622236805));
#108416=CARTESIAN_POINT('Ctrl Pts',(109.288354036607,25.6722415254375,42.7279727638635));
#108417=CARTESIAN_POINT('Ctrl Pts',(109.079161047597,25.6512330508751,42.4357219166886));
#108418=CARTESIAN_POINT('Ctrl Pts',(109.039553457205,25.6302245763126,42.1210844078894));
#108419=CARTESIAN_POINT('Ctrl Pts',(109.034533077624,25.6275616898383,42.0812031702488));
#108420=CARTESIAN_POINT('Ctrl Pts',(109.032237310398,25.624898803364,42.0409622614609));
#108421=CARTESIAN_POINT('Ctrl Pts',(109.032548003746,25.6222359168897,42.0006735849849));
#108422=CARTESIAN_POINT('Origin',(110.,24.53,42.));
#108423=CARTESIAN_POINT('',(109.034715906394,25.1642640831103,42.0001041586162));
#108424=CARTESIAN_POINT('',(109.034710481353,25.2222359168897,42.0001372498462));
#108425=CARTESIAN_POINT('',(109.03325,24.53,42.));
#108426=CARTESIAN_POINT('Ctrl Pts',(109.034715906394,25.1642640831103,42.0001041586162));
#108427=CARTESIAN_POINT('Ctrl Pts',(109.034566524345,25.1743384843849,42.1536664781764));
#108428=CARTESIAN_POINT('Ctrl Pts',(109.069123406379,25.1844128856595,42.3071651928001));
#108429=CARTESIAN_POINT('Ctrl Pts',(109.138750317064,25.1944872869341,42.4426393893168));
#108430=CARTESIAN_POINT('Ctrl Pts',(109.283945564119,25.2154957614966,42.7251481095688));
#108431=CARTESIAN_POINT('Ctrl Pts',(109.581646719205,25.236504236059,42.9292752143365));
#108432=CARTESIAN_POINT('Ctrl Pts',(109.897499355924,25.2575127106215,42.962898308317));
#108433=CARTESIAN_POINT('Ctrl Pts',(110.213351992642,25.278521185184,42.9965214022976));
#108434=CARTESIAN_POINT('Ctrl Pts',(110.547356110992,25.2995296597464,42.8596404854909));
#108435=CARTESIAN_POINT('Ctrl Pts',(110.748769062449,25.3205381343089,42.614026335183));
#108436=CARTESIAN_POINT('Ctrl Pts',(110.950182013906,25.3415466088713,42.3684121848753));
#108437=CARTESIAN_POINT('Ctrl Pts',(111.019003798469,25.3625550834338,42.0140648010663));
#108438=CARTESIAN_POINT('Ctrl Pts',(110.924180524676,25.3835635579963,41.7109157798489));
#108439=CARTESIAN_POINT('Ctrl Pts',(110.829357250883,25.4045720325587,41.4077667586315));
#108440=CARTESIAN_POINT('Ctrl Pts',(110.570888918734,25.4255805071212,41.1558161000056));
#108441=CARTESIAN_POINT('Ctrl Pts',(110.265412196082,25.4465889816837,41.068749323821));
#108442=CARTESIAN_POINT('Ctrl Pts',(109.959935473431,25.4675974562461,40.9816825476364));
#108443=CARTESIAN_POINT('Ctrl Pts',(109.607450360277,25.4886059308086,41.0594996538931));
#108444=CARTESIAN_POINT('Ctrl Pts',(109.367064504317,25.509614405371,41.2671285571739));
#108445=CARTESIAN_POINT('Ctrl Pts',(109.15862465905,25.5278309646175,41.4471646757718));
#108446=CARTESIAN_POINT('Ctrl Pts',(109.034469058168,25.5460475238639,41.7248025938681));
#108447=CARTESIAN_POINT('Ctrl Pts',(109.032306318989,25.5642640831103,42.0006908675261));
#108448=CARTESIAN_POINT('Ctrl Pts',(109.032548003746,25.6222359168897,42.0006735849849));
#108449=CARTESIAN_POINT('Ctrl Pts',(109.034688482602,25.6038903288015,41.7231103203184));
#108450=CARTESIAN_POINT('Ctrl Pts',(109.160540193731,25.5855447407134,41.4432798433115));
#108451=CARTESIAN_POINT('Ctrl Pts',(109.371468464982,25.5671991526252,41.2631720502119));
#108452=CARTESIAN_POINT('Ctrl Pts',(109.613013254922,25.5461906780628,41.056921371757));
#108453=CARTESIAN_POINT('Ctrl Pts',(109.966125026575,25.5251822035003,40.9814441852706));
#108454=CARTESIAN_POINT('Ctrl Pts',(110.271108162041,25.5041737289379,41.0704195389749));
#108455=CARTESIAN_POINT('Ctrl Pts',(110.576091297507,25.4831652543754,41.1593948926792));
#108456=CARTESIAN_POINT('Ctrl Pts',(110.832945796785,25.462156779813,41.412822786574));
#108457=CARTESIAN_POINT('Ctrl Pts',(110.925903746015,25.4411483052505,41.7165193527544));
#108458=CARTESIAN_POINT('Ctrl Pts',(111.018861695245,25.420139830688,42.0202159189348));
#108459=CARTESIAN_POINT('Ctrl Pts',(110.947923094426,25.3991313561256,42.3741811574008));
#108460=CARTESIAN_POINT('Ctrl Pts',(110.745030040548,25.3781228815631,42.6185773842525));
#108461=CARTESIAN_POINT('Ctrl Pts',(110.542136986669,25.3571144070006,42.8629736111042));
#108462=CARTESIAN_POINT('Ctrl Pts',(110.207289479731,25.3361059324382,42.9978008263417));
#108463=CARTESIAN_POINT('Ctrl Pts',(109.891642598199,25.3150974578757,42.9622525435628));
#108464=CARTESIAN_POINT('Ctrl Pts',(109.575995716666,25.2940889833133,42.926704260784));
#108465=CARTESIAN_POINT('Ctrl Pts',(109.27954946054,25.2730805087508,42.7207804799889));
#108466=CARTESIAN_POINT('Ctrl Pts',(109.136076806743,25.2520720341883,42.4373967098996));
#108467=CARTESIAN_POINT('Ctrl Pts',(109.068157121679,25.2421266617554,42.3032433649439));
#108468=CARTESIAN_POINT('Ctrl Pts',(109.034519705577,25.2321812893226,42.1517307884195));
#108469=CARTESIAN_POINT('Ctrl Pts',(109.034710481353,25.2222359168897,42.0001372498462));
#108470=CARTESIAN_POINT('Origin',(110.,24.53,42.));
#108471=CARTESIAN_POINT('',(109.032641470368,24.7642640831103,41.9992259658271));
#108472=CARTESIAN_POINT('',(109.032697715776,24.8222359168897,41.9992128726693));
#108473=CARTESIAN_POINT('',(109.03325,24.53,42.));
#108474=CARTESIAN_POINT('Ctrl Pts',(109.032641470368,24.7642640831103,41.9992259658271));
#108475=CARTESIAN_POINT('Ctrl Pts',(109.03493584802,24.7816209703435,42.2623534561074));
#108476=CARTESIAN_POINT('Ctrl Pts',(109.146410049054,24.7989778575767,42.5271931796135));
#108477=CARTESIAN_POINT('Ctrl Pts',(109.337910161716,24.8163347448098,42.7066241744067));
#108478=CARTESIAN_POINT('Ctrl Pts',(109.569698568907,24.8373432193723,42.9238043311475));
#108479=CARTESIAN_POINT('Ctrl Pts',(109.918727023337,24.8583516939348,43.0158584732588));
#108480=CARTESIAN_POINT('Ctrl Pts',(110.227475156868,24.8793601684972,42.9412415806255));
#108481=CARTESIAN_POINT('Ctrl Pts',(110.5362232904,24.9003686430597,42.8666246879923));
#108482=CARTESIAN_POINT('Ctrl Pts',(110.804691103032,24.9213771176221,42.6253367606144));
#108483=CARTESIAN_POINT('Ctrl Pts',(110.911716082052,24.9423855921846,42.3262736383281));
#108484=CARTESIAN_POINT('Ctrl Pts',(111.018741061072,24.963394066747,42.0272105160418));
#108485=CARTESIAN_POINT('Ctrl Pts',(110.964323206479,24.9844025413095,41.6703721988471));
#108486=CARTESIAN_POINT('Ctrl Pts',(110.773021965262,25.005411015872,41.4168038702247));
#108487=CARTESIAN_POINT('Ctrl Pts',(110.581720724044,25.0264194904344,41.1632355416022));
#108488=CARTESIAN_POINT('Ctrl Pts',(110.253536096201,25.0474279649969,41.012937201552));
#108489=CARTESIAN_POINT('Ctrl Pts',(109.936581269547,25.0684364395594,41.033739887542));
#108490=CARTESIAN_POINT('Ctrl Pts',(109.619626442893,25.0894449141218,41.054542573532));
#108491=CARTESIAN_POINT('Ctrl Pts',(109.313901417428,25.1104533886843,41.2464462855623));
#108492=CARTESIAN_POINT('Ctrl Pts',(109.157383574207,25.1314618632467,41.5228433094456));
#108493=CARTESIAN_POINT('Ctrl Pts',(109.075922278026,25.1423959365346,41.6666969389274));
#108494=CARTESIAN_POINT('Ctrl Pts',(109.03487803556,25.1533300098225,41.8334380103697));
#108495=CARTESIAN_POINT('Ctrl Pts',(109.034715906394,25.1642640831103,42.0001041586162));
#108496=CARTESIAN_POINT('Ctrl Pts',(109.034710481353,25.2222359168897,42.0001372498462));
#108497=CARTESIAN_POINT('Ctrl Pts',(109.03492269783,25.2111728147601,41.8315065815894));
#108498=CARTESIAN_POINT('Ctrl Pts',(109.076994075968,25.2001097126305,41.6627757305176));
#108499=CARTESIAN_POINT('Ctrl Pts',(109.160299591046,25.1890466105009,41.5177277634241));
#108500=CARTESIAN_POINT('Ctrl Pts',(109.318494080615,25.1680381359385,41.2422863464211));
#108501=CARTESIAN_POINT('Ctrl Pts',(109.62538211122,25.147029661376,41.0522472717984));
#108502=CARTESIAN_POINT('Ctrl Pts',(109.942458023974,25.1260211868136,41.0333727242458));
#108503=CARTESIAN_POINT('Ctrl Pts',(110.259533936729,25.1050127122511,41.0144981766932));
#108504=CARTESIAN_POINT('Ctrl Pts',(110.586797731632,25.0840042376886,41.1667881562108));
#108505=CARTESIAN_POINT('Ctrl Pts',(110.776553416921,25.0629957631262,41.4215146740517));
#108506=CARTESIAN_POINT('Ctrl Pts',(110.966309102209,25.0419872885637,41.6762411918927));
#108507=CARTESIAN_POINT('Ctrl Pts',(111.018556677882,25.0209788140013,42.033404248057));
#108508=CARTESIAN_POINT('Ctrl Pts',(110.909715401718,24.9999703394388,42.3318112002329));
#108509=CARTESIAN_POINT('Ctrl Pts',(110.800874125554,24.9789618648763,42.6302181524088));
#108510=CARTESIAN_POINT('Ctrl Pts',(110.530943997553,24.9579533903139,42.8698690005962));
#108511=CARTESIAN_POINT('Ctrl Pts',(110.221747852986,24.9369449157514,42.9426071642036));
#108512=CARTESIAN_POINT('Ctrl Pts',(109.912551708419,24.915936441189,43.015345327811));
#108513=CARTESIAN_POINT('Ctrl Pts',(109.564089547287,24.8949279666265,42.9211708068382));
#108514=CARTESIAN_POINT('Ctrl Pts',(109.33362599082,24.873919492064,42.7025853689385));
#108515=CARTESIAN_POINT('Ctrl Pts',(109.144635900016,24.8566916336726,42.523335849447));
#108516=CARTESIAN_POINT('Ctrl Pts',(109.034996446688,24.8394637752811,42.2604235985598));
#108517=CARTESIAN_POINT('Ctrl Pts',(109.032697715776,24.8222359168897,41.9992128726693));
#108518=CARTESIAN_POINT('Origin',(110.,24.53,42.));
#108519=CARTESIAN_POINT('',(109.032632519022,24.3642640831103,42.0007718204176));
#108520=CARTESIAN_POINT('',(109.032577150836,24.4222359168897,42.0007573162032));
#108521=CARTESIAN_POINT('',(109.03325,24.53,42.));
#108522=CARTESIAN_POINT('Ctrl Pts',(109.032632519022,24.3642640831103,42.0007718204176));
#108523=CARTESIAN_POINT('Ctrl Pts',(109.032153349384,24.3678949817396,42.0558143102464));
#108524=CARTESIAN_POINT('Ctrl Pts',(109.03645356453,24.3715258803689,42.1107819869543));
#108525=CARTESIAN_POINT('Ctrl Pts',(109.045800826623,24.3751567789982,42.1648775768284));
#108526=CARTESIAN_POINT('Ctrl Pts',(109.099884329895,24.3961652535606,42.477876076607));
#108527=CARTESIAN_POINT('Ctrl Pts',(109.322933370855,24.4171737281231,42.7616787669617));
#108528=CARTESIAN_POINT('Ctrl Pts',(109.61428345485,24.4381822026855,42.8882023557283));
#108529=CARTESIAN_POINT('Ctrl Pts',(109.905633538845,24.459190677248,43.0147259444948));
#108530=CARTESIAN_POINT('Ctrl Pts',(110.265284665876,24.4801991518105,42.9839704316732));
#108531=CARTESIAN_POINT('Ctrl Pts',(110.530922326302,24.5012076263729,42.8098161254884));
#108532=CARTESIAN_POINT('Ctrl Pts',(110.796559986728,24.5222161009354,42.6356618193037));
#108533=CARTESIAN_POINT('Ctrl Pts',(110.968184180549,24.5432245754978,42.3181087197559));
#108534=CARTESIAN_POINT('Ctrl Pts',(110.968339017755,24.5642330500603,42.000472032944));
#108535=CARTESIAN_POINT('Ctrl Pts',(110.96849385496,24.5852415246228,41.6828353461321));
#108536=CARTESIAN_POINT('Ctrl Pts',(110.79717933555,24.6062499991852,41.3651150720561));
#108537=CARTESIAN_POINT('Ctrl Pts',(110.531711589679,24.6272584737477,41.1907018710498));
#108538=CARTESIAN_POINT('Ctrl Pts',(110.266243843807,24.6482669483101,41.0162886700435));
#108539=CARTESIAN_POINT('Ctrl Pts',(109.906622871474,24.6692754228726,40.9851825421069));
#108540=CARTESIAN_POINT('Ctrl Pts',(109.615149574554,24.6902838974351,41.1114220215978));
#108541=CARTESIAN_POINT('Ctrl Pts',(109.323676277635,24.7112923719975,41.2376615010887));
#108542=CARTESIAN_POINT('Ctrl Pts',(109.100350656129,24.73230084656,41.5212465880071));
#108543=CARTESIAN_POINT('Ctrl Pts',(109.045962025352,24.7533093211224,41.8341922171514));
#108544=CARTESIAN_POINT('Ctrl Pts',(109.036508467246,24.7569609084517,41.8885868515997));
#108545=CARTESIAN_POINT('Ctrl Pts',(109.032158773197,24.760612495781,41.9438685162689));
#108546=CARTESIAN_POINT('Ctrl Pts',(109.032641470368,24.7642640831103,41.9992259658271));
#108547=CARTESIAN_POINT('Ctrl Pts',(109.032697715776,24.8222359168897,41.9992128726693));
#108548=CARTESIAN_POINT('Ctrl Pts',(109.032193264262,24.8184553007187,41.9418907452229));
#108549=CARTESIAN_POINT('Ctrl Pts',(109.036858057582,24.8146746845477,41.8846505587128));
#108550=CARTESIAN_POINT('Ctrl Pts',(109.046987895688,24.8108940683766,41.8283944448405));
#108551=CARTESIAN_POINT('Ctrl Pts',(109.103278308826,24.7898855938142,41.5157853134692));
#108552=CARTESIAN_POINT('Ctrl Pts',(109.328324086905,24.7688771192517,41.2335634055532));
#108553=CARTESIAN_POINT('Ctrl Pts',(109.620559550287,24.7478686446893,41.109098523204));
#108554=CARTESIAN_POINT('Ctrl Pts',(109.91279501367,24.7268601701268,40.9846336408548));
#108555=CARTESIAN_POINT('Ctrl Pts',(110.272220162357,24.7058516955644,41.0179257840723));
#108556=CARTESIAN_POINT('Ctrl Pts',(110.536622489988,24.6848432210019,41.1939498668055));
#108557=CARTESIAN_POINT('Ctrl Pts',(110.80102481762,24.6638347464394,41.3699739495386));
#108558=CARTESIAN_POINT('Ctrl Pts',(110.970404324194,24.642826271877,41.6887299717873));
#108559=CARTESIAN_POINT('Ctrl Pts',(110.968318164027,24.6218177973145,42.0063598196718));
#108560=CARTESIAN_POINT('Ctrl Pts',(110.966232003859,24.600809322752,42.3239896675563));
#108561=CARTESIAN_POINT('Ctrl Pts',(110.792680176949,24.5798008481896,42.6404933410765));
#108562=CARTESIAN_POINT('Ctrl Pts',(110.525988538177,24.5587923736271,42.8130292538006));
#108563=CARTESIAN_POINT('Ctrl Pts',(110.259296899404,24.5377838990647,42.9855651665247));
#108564=CARTESIAN_POINT('Ctrl Pts',(109.89946544877,24.5167754245022,43.0141333184527));
#108565=CARTESIAN_POINT('Ctrl Pts',(109.608890078749,24.4957669499397,42.8858405848606));
#108566=CARTESIAN_POINT('Ctrl Pts',(109.318314708729,24.4747584753773,42.7575478512684));
#108567=CARTESIAN_POINT('Ctrl Pts',(109.096995419324,24.4537500008148,42.4723942321562));
#108568=CARTESIAN_POINT('Ctrl Pts',(109.044816044342,24.4327415262524,42.1590726976564));
#108569=CARTESIAN_POINT('Ctrl Pts',(109.036118345885,24.4292396564648,42.1068456208073));
#108570=CARTESIAN_POINT('Ctrl Pts',(109.032120205872,24.4257377866772,42.0538358974429));
#108571=CARTESIAN_POINT('Ctrl Pts',(109.032577150836,24.4222359168897,42.0007573162032));
#108572=CARTESIAN_POINT('Origin',(110.,24.53,42.));
#108573=CARTESIAN_POINT('',(109.034717052885,23.9642640831103,41.9999017201984));
#108574=CARTESIAN_POINT('',(109.034721981614,24.0222359168897,41.9999322711442));
#108575=CARTESIAN_POINT('',(109.03325,24.53,42.));
#108576=CARTESIAN_POINT('Ctrl Pts',(109.034717052885,23.9642640831103,41.9999017201984));
#108577=CARTESIAN_POINT('Ctrl Pts',(109.034871038885,23.9751774676982,42.1662525240113));
#108578=CARTESIAN_POINT('Ctrl Pts',(109.075751609479,23.986090852286,42.3326741490512));
#108579=CARTESIAN_POINT('Ctrl Pts',(109.156918704901,23.9970042368738,42.4763345202534));
#108580=CARTESIAN_POINT('Ctrl Pts',(109.313166919719,24.0180127114363,42.7528834890671));
#108581=CARTESIAN_POINT('Ctrl Pts',(109.618704861746,24.0390211859988,42.9450861065659));
#108582=CARTESIAN_POINT('Ctrl Pts',(109.935639297263,24.0600296605612,42.9661980378269));
#108583=CARTESIAN_POINT('Ctrl Pts',(110.25257373278,24.0810381351237,42.987309969088));
#108584=CARTESIAN_POINT('Ctrl Pts',(110.580904661786,24.1020466096862,42.8373312141113));
#108585=CARTESIAN_POINT('Ctrl Pts',(110.772453004619,24.1230550842486,42.5839493950286));
#108586=CARTESIAN_POINT('Ctrl Pts',(110.964001347452,24.1440635588111,42.330567575946));
#108587=CARTESIAN_POINT('Ctrl Pts',(111.018767104112,24.1650720333735,41.9737826927573));
#108588=CARTESIAN_POINT('Ctrl Pts',(110.912033751289,24.186080507936,41.6746154258864));
#108589=CARTESIAN_POINT('Ctrl Pts',(110.805300398467,24.2070889824985,41.3754481590154));
#108590=CARTESIAN_POINT('Ctrl Pts',(110.537067936161,24.2280974570609,41.1338985084622));
#108591=CARTESIAN_POINT('Ctrl Pts',(110.228392691396,24.2491059316234,41.0589806166415));
#108592=CARTESIAN_POINT('Ctrl Pts',(109.91971744663,24.2701144061858,40.9840627248208));
#108593=CARTESIAN_POINT('Ctrl Pts',(109.570599419405,24.2911228807483,41.0757765917327));
#108594=CARTESIAN_POINT('Ctrl Pts',(109.338599388585,24.3121313553108,41.2927306797899));
#108595=CARTESIAN_POINT('Ctrl Pts',(109.14669596694,24.329508931244,41.4721885518035));
#108596=CARTESIAN_POINT('Ctrl Pts',(109.034925837462,24.3468865071771,41.7373370225303));
#108597=CARTESIAN_POINT('Ctrl Pts',(109.032632519022,24.3642640831103,42.0007718204176));
#108598=CARTESIAN_POINT('Ctrl Pts',(109.032577150836,24.4222359168897,42.0007573162032));
#108599=CARTESIAN_POINT('Ctrl Pts',(109.03486151758,24.4047293121148,41.7354060038618));
#108600=CARTESIAN_POINT('Ctrl Pts',(109.148488100179,24.3872227073399,41.4683337841834));
#108601=CARTESIAN_POINT('Ctrl Pts',(109.342912081085,24.369716102565,41.288722292881));
#108602=CARTESIAN_POINT('Ctrl Pts',(109.57622695337,24.3487076280025,41.0731828724926));
#108603=CARTESIAN_POINT('Ctrl Pts',(109.925896158499,24.3276991534401,40.983593481603));
#108604=CARTESIAN_POINT('Ctrl Pts',(110.234110139142,24.3066906788776,41.0603868046682));
#108605=CARTESIAN_POINT('Ctrl Pts',(110.542324119785,24.2856822043151,41.1371801277335));
#108606=CARTESIAN_POINT('Ctrl Pts',(110.809082875943,24.2646737297527,41.3803561647535));
#108607=CARTESIAN_POINT('Ctrl Pts',(110.913995235129,24.2436652551902,41.6801668807872));
#108608=CARTESIAN_POINT('Ctrl Pts',(111.018907594316,24.2226567806277,41.9799775968209));
#108609=CARTESIAN_POINT('Ctrl Pts',(110.961973556532,24.2016483060653,42.3364229918684));
#108610=CARTESIAN_POINT('Ctrl Pts',(110.768888098739,24.1806398315028,42.5886353606882));
#108611=CARTESIAN_POINT('Ctrl Pts',(110.575802640947,24.1596313569404,42.8408477295081));
#108612=CARTESIAN_POINT('Ctrl Pts',(110.246565763145,24.1386228823779,42.9888270721004));
#108613=CARTESIAN_POINT('Ctrl Pts',(109.929765653102,24.1176144078154,42.9657886280353));
#108614=CARTESIAN_POINT('Ctrl Pts',(109.612965543059,24.096605933253,42.9427501839702));
#108615=CARTESIAN_POINT('Ctrl Pts',(109.308602200776,24.0755974586905,42.7486939532477));
#108616=CARTESIAN_POINT('Ctrl Pts',(109.154038237157,24.0545889841281,42.4711997629087));
#108617=CARTESIAN_POINT('Ctrl Pts',(109.07469536225,24.0438046283819,42.3287526729402));
#108618=CARTESIAN_POINT('Ctrl Pts',(109.034826328108,24.0330202726358,42.1643187312172));
#108619=CARTESIAN_POINT('Ctrl Pts',(109.034721981614,24.0222359168897,41.9999322711442));
#108620=CARTESIAN_POINT('Origin',(110.,24.53,42.));
#108621=CARTESIAN_POINT('',(109.032328989546,23.5642640831103,41.9994138103573));
#108622=CARTESIAN_POINT('',(109.032351030732,23.6222359168897,41.9993265593643));
#108623=CARTESIAN_POINT('',(109.03325,24.53,42.));
#108624=CARTESIAN_POINT('Ctrl Pts',(109.032328989546,23.5642640831103,41.9994138103573));
#108625=CARTESIAN_POINT('Ctrl Pts',(109.034503741766,23.5824599536567,42.2750214683126));
#108626=CARTESIAN_POINT('Ctrl Pts',(109.158321797255,23.6006558242031,42.5522194353554));
#108627=CARTESIAN_POINT('Ctrl Pts',(109.366343274976,23.6188516947496,42.7322146822975));
#108628=CARTESIAN_POINT('Ctrl Pts',(109.606519413403,23.639860169312,42.9400324702457));
#108629=CARTESIAN_POINT('Ctrl Pts',(109.958942128383,23.6608686438745,43.018275090416));
#108630=CARTESIAN_POINT('Ctrl Pts',(110.264507194704,23.6818771184369,42.9315276900637));
#108631=CARTESIAN_POINT('Ctrl Pts',(110.570072261024,23.7028855929994,42.8447802897114));
#108632=CARTESIAN_POINT('Ctrl Pts',(110.828779678684,23.7238940675619,42.5930428688364));
#108633=CARTESIAN_POINT('Ctrl Pts',(110.923896771461,23.7449025421243,42.2899762255731));
#108634=CARTESIAN_POINT('Ctrl Pts',(111.019013864237,23.7659110166868,41.9869095823098));
#108635=CARTESIAN_POINT('Ctrl Pts',(110.95054063213,23.7869194912492,41.6325137166583));
#108636=CARTESIAN_POINT('Ctrl Pts',(110.749368036451,23.8079279658117,41.3867081653265));
#108637=CARTESIAN_POINT('Ctrl Pts',(110.548195440771,23.8289364403742,41.1409026139947));
#108638=CARTESIAN_POINT('Ctrl Pts',(110.21432348152,23.8499449149366,41.0036873769827));
#108639=CARTESIAN_POINT('Ctrl Pts',(109.898437833994,23.8709533894991,41.0370002203453));
#108640=CARTESIAN_POINT('Ctrl Pts',(109.582552186467,23.8919618640615,41.0703130637079));
#108641=CARTESIAN_POINT('Ctrl Pts',(109.284652850666,23.912970338624,41.2741539874452));
#108642=CARTESIAN_POINT('Ctrl Pts',(109.13918242657,23.9339788131865,41.5565221093782));
#108643=CARTESIAN_POINT('Ctrl Pts',(109.069280301334,23.9440739031611,41.6922069535301));
#108644=CARTESIAN_POINT('Ctrl Pts',(109.034574612883,23.9541689931357,41.8460240374021));
#108645=CARTESIAN_POINT('Ctrl Pts',(109.034717052885,23.9642640831103,41.9999017201984));
#108646=CARTESIAN_POINT('Ctrl Pts',(109.034721981614,24.0222359168897,41.9999322711442));
#108647=CARTESIAN_POINT('Ctrl Pts',(109.034623055819,24.0120117980733,41.8440855298878));
#108648=CARTESIAN_POINT('Ctrl Pts',(109.070264656034,24.001787679257,41.688281465168));
#108649=CARTESIAN_POINT('Ctrl Pts',(109.141894615443,23.9915635604407,41.5512957262226));
#108650=CARTESIAN_POINT('Ctrl Pts',(109.2890795423,23.9705550858782,41.2698180298312));
#108651=CARTESIAN_POINT('Ctrl Pts',(109.588213980968,23.9495466113158,41.0677947870039));
#108652=CARTESIAN_POINT('Ctrl Pts',(109.904295637963,23.9285381367533,41.0364018162067));
#108653=CARTESIAN_POINT('Ctrl Pts',(110.220377294958,23.9075296621908,41.0050088454096));
#108654=CARTESIAN_POINT('Ctrl Pts',(110.553406170279,23.8865211876284,41.1442461466425));
#108655=CARTESIAN_POINT('Ctrl Pts',(110.753081882588,23.8655127130659,41.3912733291643));
#108656=CARTESIAN_POINT('Ctrl Pts',(110.952757594896,23.8445042385035,41.638300511686));
#108657=CARTESIAN_POINT('Ctrl Pts',(111.019080144193,23.823495763941,41.9931175754965));
#108658=CARTESIAN_POINT('Ctrl Pts',(110.922119084851,23.8024872893785,42.2955939150102));
#108659=CARTESIAN_POINT('Ctrl Pts',(110.825158025509,23.7814788148161,42.5980702545239));
#108660=CARTESIAN_POINT('Ctrl Pts',(110.564913357529,23.7604703402536,42.8482058697408));
#108661=CARTESIAN_POINT('Ctrl Pts',(110.258832885919,23.7394618656911,42.9331070807446));
#108662=CARTESIAN_POINT('Ctrl Pts',(109.95275241431,23.7184533911287,43.0180082917484));
#108663=CARTESIAN_POINT('Ctrl Pts',(109.600836139072,23.6974449165662,42.9376750985392));
#108664=CARTESIAN_POINT('Ctrl Pts',(109.361915079957,23.6764364420038,42.7283727071308));
#108665=CARTESIAN_POINT('Ctrl Pts',(109.156448046066,23.6583696002991,42.5483770980853));
#108666=CARTESIAN_POINT('Ctrl Pts',(109.034548144198,23.6403027585944,42.2730005837007));
#108667=CARTESIAN_POINT('Ctrl Pts',(109.032351030732,23.6222359168897,41.9993265593643));
#108668=CARTESIAN_POINT('Origin',(110.,26.4327725593024,42.));
#108669=CARTESIAN_POINT('',(109.26029596408,23.4327725593024,41.9995519067537));
#108670=CARTESIAN_POINT('',(109.261,23.36675,42.));
#108671=CARTESIAN_POINT('',(109.261,26.4327725593024,42.));
#108672=CARTESIAN_POINT('',(109.624043822086,23.36675,41.3637783780095));
#108673=CARTESIAN_POINT('Ctrl Pts',(109.26029596408,23.4327725593024,41.9995519067537));
#108674=CARTESIAN_POINT('Ctrl Pts',(109.260038998003,23.4299599552863,41.9669864411116));
#108675=CARTESIAN_POINT('Ctrl Pts',(109.275412450265,23.4079524355189,41.7124017577352));
#108676=CARTESIAN_POINT('Ctrl Pts',(109.433281110202,23.3859449157514,41.4766714936968));
#108677=CARTESIAN_POINT('Ctrl Pts',(109.623765654177,23.36675,41.3626306739548));
#108678=CARTESIAN_POINT('Origin',(110.,23.36675,42.));
#108679=CARTESIAN_POINT('Origin',(110.,26.4327725593024,42.));
#108680=CARTESIAN_POINT('',(109.262121439961,23.8327725593024,41.9999248732626));
#108681=CARTESIAN_POINT('',(109.260312812734,23.7537274406976,41.9994852106234));
#108682=CARTESIAN_POINT('',(109.261,26.4327725593024,42.));
#108683=CARTESIAN_POINT('Ctrl Pts',(109.262121439961,23.8327725593024,41.9999248732626));
#108684=CARTESIAN_POINT('Ctrl Pts',(109.262012556422,23.8226774693278,41.8822981780607));
#108685=CARTESIAN_POINT('Ctrl Pts',(109.343751851955,23.7915739047907,41.5200261518318));
#108686=CARTESIAN_POINT('Ctrl Pts',(109.908615127961,23.7394618656911,41.1335121918162));
#108687=CARTESIAN_POINT('Ctrl Pts',(110.674267192777,23.6764364420038,41.4481811139323));
#108688=CARTESIAN_POINT('Ctrl Pts',(110.831293472147,23.6134110183164,42.2608996390416));
#108689=CARTESIAN_POINT('Ctrl Pts',(110.23801253607,23.550385594629,42.8381966259357));
#108690=CARTESIAN_POINT('Ctrl Pts',(109.465885790711,23.4901727749577,42.6667740215107));
#108691=CARTESIAN_POINT('Ctrl Pts',(109.261958381344,23.4509684298488,42.2102310474094));
#108692=CARTESIAN_POINT('Ctrl Pts',(109.26029596408,23.4327725593024,41.9995519067537));
#108693=CARTESIAN_POINT('',(109.276407492811,23.36675,42.1501162334309));
#108694=CARTESIAN_POINT('Origin',(110.,23.36675,42.));
#108695=CARTESIAN_POINT('Ctrl Pts',(109.260312812734,23.7537274406976,41.9994852106234));
#108696=CARTESIAN_POINT('Ctrl Pts',(109.26003935578,23.7507858078399,41.9654232168984));
#108697=CARTESIAN_POINT('Ctrl Pts',(109.277562880338,23.7268357004196,41.6883790874115));
#108698=CARTESIAN_POINT('Ctrl Pts',(109.627143274457,23.6818771184369,41.2124713920096));
#108699=CARTESIAN_POINT('Ctrl Pts',(110.453854470857,23.6188516947496,41.2562957542224));
#108700=CARTESIAN_POINT('Ctrl Pts',(110.870694764692,23.5558262710622,41.9711141768508));
#108701=CARTESIAN_POINT('Ctrl Pts',(110.502088724856,23.4928008473748,42.7126144441227));
#108702=CARTESIAN_POINT('Ctrl Pts',(109.679417589571,23.4297754236874,42.8095875279876));
#108703=CARTESIAN_POINT('Ctrl Pts',(109.325945901895,23.3877584745625,42.3889020117039));
#108704=CARTESIAN_POINT('Ctrl Pts',(109.276407492811,23.36675,42.1501162334309));
#108705=CARTESIAN_POINT('Origin',(110.,26.4327725593024,42.));
#108706=CARTESIAN_POINT('',(109.26052798713,24.2327725593024,42.0005899925406));
#108707=CARTESIAN_POINT('',(109.262125207564,24.1537274406976,41.9999482269207));
#108708=CARTESIAN_POINT('',(109.261,26.4327725593024,42.));
#108709=CARTESIAN_POINT('Ctrl Pts',(109.26052798713,24.2327725593024,42.0005899925406));
#108710=CARTESIAN_POINT('Ctrl Pts',(109.262281038411,24.2153949833692,41.7992159913627));
#108711=CARTESIAN_POINT('Ctrl Pts',(109.451010737328,24.1770089328736,41.3514989556746));
#108712=CARTESIAN_POINT('Ctrl Pts',(110.205502368947,24.1176144078154,41.1532927913056));
#108713=CARTESIAN_POINT('Ctrl Pts',(110.820626619199,24.0545889841281,41.7072266679816));
#108714=CARTESIAN_POINT('Ctrl Pts',(110.695035015874,23.9915635604407,42.525423808948));
#108715=CARTESIAN_POINT('Ctrl Pts',(109.942089921891,23.9285381367533,42.8693626760629));
#108716=CARTESIAN_POINT('Ctrl Pts',(109.353645406068,23.8756078030405,42.4991939976866));
#108717=CARTESIAN_POINT('Ctrl Pts',(109.262239149456,23.8436859438902,42.1270862324741));
#108718=CARTESIAN_POINT('Ctrl Pts',(109.262121439961,23.8327725593024,41.9999248732626));
#108719=CARTESIAN_POINT('Ctrl Pts',(109.262125207564,24.1537274406976,41.9999482269206));
#108720=CARTESIAN_POINT('Ctrl Pts',(109.262049587019,24.1435033218813,41.8808163502323));
#108721=CARTESIAN_POINT('Ctrl Pts',(109.345277616316,24.1122707285025,41.5169924706903));
#108722=CARTESIAN_POINT('Ctrl Pts',(109.913887232595,24.0600296605612,41.1329766445788));
#108723=CARTESIAN_POINT('Ctrl Pts',(110.677605894697,23.9970042368739,41.452282666646));
#108724=CARTESIAN_POINT('Ctrl Pts',(110.82970011946,23.9339788131865,42.2659671046784));
#108725=CARTESIAN_POINT('Ctrl Pts',(110.232893883192,23.8709533894991,42.839590749815));
#108726=CARTESIAN_POINT('Ctrl Pts',(109.463528899382,23.8108695986695,42.663965039265));
#108727=CARTESIAN_POINT('Ctrl Pts',(109.261992323312,23.7717942824023,42.2086862491387));
#108728=CARTESIAN_POINT('Ctrl Pts',(109.260312812734,23.7537274406976,41.9994852106234));
#108729=CARTESIAN_POINT('Origin',(110.,26.4327725593024,42.));
#108730=CARTESIAN_POINT('',(109.260534829689,24.6327725593024,41.9994083152275));
#108731=CARTESIAN_POINT('',(109.260485662754,24.5537274406976,42.0005789052745));
#108732=CARTESIAN_POINT('',(109.261,26.4327725593024,42.));
#108733=CARTESIAN_POINT('Ctrl Pts',(109.260534829689,24.6327725593024,41.9994083152275));
#108734=CARTESIAN_POINT('Ctrl Pts',(109.260165847833,24.6291209719731,41.9570921474246));
#108735=CARTESIAN_POINT('Ctrl Pts',(109.282620247005,24.6044609100813,41.6717119456296));
#108736=CARTESIAN_POINT('Ctrl Pts',(109.653720613876,24.5587923736271,41.2004783760763));
#108737=CARTESIAN_POINT('Ctrl Pts',(110.478421617924,24.4957669499397,41.271812522066));
#108738=CARTESIAN_POINT('Ctrl Pts',(110.871288739239,24.4327415262524,42.0004247254552));
#108739=CARTESIAN_POINT('Ctrl Pts',(110.4777114569,24.369716102565,42.7286535557603));
#108740=CARTESIAN_POINT('Ctrl Pts',(109.652941300575,24.3066906788776,42.7991836534335));
#108741=CARTESIAN_POINT('Ctrl Pts',(109.282468435015,24.2610428311234,42.32780213349));
#108742=CARTESIAN_POINT('Ctrl Pts',(109.260161701779,24.2364034579317,42.042665399816));
#108743=CARTESIAN_POINT('Ctrl Pts',(109.26052798713,24.2327725593024,42.0005899925406));
#108744=CARTESIAN_POINT('Ctrl Pts',(109.260485662754,24.5537274406976,42.0005789052745));
#108745=CARTESIAN_POINT('Ctrl Pts',(109.262231871209,24.5362208359227,41.7977398881343));
#108746=CARTESIAN_POINT('Ctrl Pts',(109.453322360428,24.4977057565854,41.3485935708913));
#108747=CARTESIAN_POINT('Ctrl Pts',(110.210646810159,24.4381822026855,41.1545580791696));
#108748=CARTESIAN_POINT('Ctrl Pts',(110.822391482929,24.3751567789981,41.7122216675569));
#108749=CARTESIAN_POINT('Ctrl Pts',(110.691827467654,24.3121313553108,42.5296402771459));
#108750=CARTESIAN_POINT('Ctrl Pts',(109.93680480607,24.2491059316234,42.8689939906469));
#108751=CARTESIAN_POINT('Ctrl Pts',(109.352051429389,24.1963046267523,42.49616645061));
#108752=CARTESIAN_POINT('Ctrl Pts',(109.262204971784,24.1645117964438,42.1256080086574));
#108753=CARTESIAN_POINT('Ctrl Pts',(109.262125207564,24.1537274406976,41.9999482269206));
#108754=CARTESIAN_POINT('Origin',(110.,26.4327725593024,42.));
#108755=CARTESIAN_POINT('',(109.262120563564,25.0327725593024,42.0000796206024));
#108756=CARTESIAN_POINT('',(109.260577824628,24.9537274406976,41.9993983065969));
#108757=CARTESIAN_POINT('',(109.261,26.4327725593024,42.));
#108758=CARTESIAN_POINT('Ctrl Pts',(109.262120563564,25.0327725593024,42.0000796206024));
#108759=CARTESIAN_POINT('Ctrl Pts',(109.262244497832,25.0218384860145,41.872677206789));
#108760=CARTESIAN_POINT('Ctrl Pts',(109.353902434325,24.9898959381642,41.5003194382249));
#108761=CARTESIAN_POINT('Ctrl Pts',(109.942937403792,24.9369449157514,41.1305819691232));
#108762=CARTESIAN_POINT('Ctrl Pts',(110.695546992547,24.873919492064,41.4752537248938));
#108763=CARTESIAN_POINT('Ctrl Pts',(110.820340769253,24.8108940683766,42.2935734034257));
#108764=CARTESIAN_POINT('Ctrl Pts',(110.204676801728,24.7478686446893,42.8469070832775));
#108765=CARTESIAN_POINT('Ctrl Pts',(109.450641491291,24.6884948083312,42.6480348344885));
#108766=CARTESIAN_POINT('Ctrl Pts',(109.262288690651,24.6501294465356,42.2005474052893));
#108767=CARTESIAN_POINT('Ctrl Pts',(109.260534829689,24.6327725593024,41.9994083152275));
#108768=CARTESIAN_POINT('Ctrl Pts',(109.260577824628,24.9537274406976,41.9993983065969));
#108769=CARTESIAN_POINT('Ctrl Pts',(109.260192213384,24.9499468245266,41.9555803058905));
#108770=CARTESIAN_POINT('Ctrl Pts',(109.28357308373,24.9251577337931,41.6686811256762));
#108771=CARTESIAN_POINT('Ctrl Pts',(109.658588394334,24.8793601684972,41.1983877597661));
#108772=CARTESIAN_POINT('Ctrl Pts',(110.482840325691,24.8163347448098,41.2747349865707));
#108773=CARTESIAN_POINT('Ctrl Pts',(110.871269977697,24.7533093211224,42.0057224200596));
#108774=CARTESIAN_POINT('Ctrl Pts',(110.473272149655,24.6902838974351,42.7315446535164));
#108775=CARTESIAN_POINT('Ctrl Pts',(109.64808846612,24.6272584737477,42.7970585845476));
#108776=CARTESIAN_POINT('Ctrl Pts',(109.281527690817,24.5817396548352,42.3247719981271));
#108777=CARTESIAN_POINT('Ctrl Pts',(109.26013636632,24.5572293104852,42.0411530677117));
#108778=CARTESIAN_POINT('Ctrl Pts',(109.260485662754,24.5537274406976,42.0005789052745));
#108779=CARTESIAN_POINT('Origin',(110.,26.4327725593024,42.));
#108780=CARTESIAN_POINT('',(109.260278634324,25.4327725593024,42.0005281107854));
#108781=CARTESIAN_POINT('',(109.262116416571,25.3537274406976,42.0001049160966));
#108782=CARTESIAN_POINT('',(109.261,26.4327725593024,42.));
#108783=CARTESIAN_POINT('Ctrl Pts',(109.260278634324,25.4327725593024,42.0005281107854));
#108784=CARTESIAN_POINT('Ctrl Pts',(109.261931868618,25.414556000056,41.7896344627551));
#108785=CARTESIAN_POINT('Ctrl Pts',(109.466290765521,25.3753309662471,41.3326451825462));
#108786=CARTESIAN_POINT('Ctrl Pts',(110.238819563989,25.3150974578757,41.1620962618873));
#108787=CARTESIAN_POINT('Ctrl Pts',(110.831552217079,25.2520720341883,41.7398822563778));
#108788=CARTESIAN_POINT('Ctrl Pts',(110.673726619585,25.1890466105009,42.5524896004734));
#108789=CARTESIAN_POINT('Ctrl Pts',(109.907771480839,25.1260211868136,42.866391842584));
#108790=CARTESIAN_POINT('Ctrl Pts',(109.343508090084,25.073929836414,42.4794889021236));
#108791=CARTESIAN_POINT('Ctrl Pts',(109.262006373407,25.042846960577,42.1174652468295));
#108792=CARTESIAN_POINT('Ctrl Pts',(109.262120563564,25.0327725593024,42.0000796206024));
#108793=CARTESIAN_POINT('Ctrl Pts',(109.262116416571,25.3537274406976,42.0001049160966));
#108794=CARTESIAN_POINT('Ctrl Pts',(109.262278638424,25.342664338568,41.8712007900642));
#108795=CARTESIAN_POINT('Ctrl Pts',(109.355509647679,25.310592761876,41.4972898740467));
#108796=CARTESIAN_POINT('Ctrl Pts',(109.948226154444,25.2575127106215,41.130252762051));
#108797=CARTESIAN_POINT('Ctrl Pts',(110.698724042524,25.1944872869341,41.479491846189));
#108798=CARTESIAN_POINT('Ctrl Pts',(110.818540825836,25.1314618632468,42.298556232552));
#108799=CARTESIAN_POINT('Ctrl Pts',(110.19952340274,25.0684364395593,42.8481356795978));
#108800=CARTESIAN_POINT('Ctrl Pts',(109.448347483645,25.009191632043,42.6451247354048));
#108801=CARTESIAN_POINT('Ctrl Pts',(109.262335013295,24.9709552990891,42.1990721896413));
#108802=CARTESIAN_POINT('Ctrl Pts',(109.260577824628,24.9537274406976,41.9993983065969));
#108803=CARTESIAN_POINT('Origin',(110.,23.36675,42.));
#108804=CARTESIAN_POINT('',(110.966013043313,23.36675,41.9622592706773));
#108805=CARTESIAN_POINT('Ctrl Pts',(109.623765654177,23.36675,41.3626306739548));
#108806=CARTESIAN_POINT('Ctrl Pts',(109.640283077264,23.36675,41.3490485696045));
#108807=CARTESIAN_POINT('Ctrl Pts',(109.657385440225,23.36675,41.3362594125259));
#108808=CARTESIAN_POINT('Ctrl Pts',(109.675032430314,23.36675,41.32431606363));
#108809=CARTESIAN_POINT('Ctrl Pts',(109.702587947937,23.36675,41.3056666985359));
#108810=CARTESIAN_POINT('Ctrl Pts',(109.731469510825,23.36675,41.2890775093067));
#108811=CARTESIAN_POINT('Ctrl Pts',(109.761429487403,23.36675,41.2745065051108));
#108812=CARTESIAN_POINT('Ctrl Pts',(109.770540279536,23.36675,41.2700754806055));
#108813=CARTESIAN_POINT('Ctrl Pts',(109.779751057641,23.36675,41.2658313065101));
#108814=CARTESIAN_POINT('Ctrl Pts',(109.789055479984,23.36675,41.2617733906582));
#108815=CARTESIAN_POINT('Ctrl Pts',(109.797186423754,23.36675,41.2582272612589));
#108816=CARTESIAN_POINT('Ctrl Pts',(109.805387488184,23.36675,41.254824141658));
#108817=CARTESIAN_POINT('Ctrl Pts',(109.813642892422,23.36675,41.2515677867019));
#108818=CARTESIAN_POINT('Ctrl Pts',(109.846811880316,23.36675,41.2384842362177));
#108819=CARTESIAN_POINT('Ctrl Pts',(109.880903278198,23.36675,41.2277454904922));
#108820=CARTESIAN_POINT('Ctrl Pts',(109.91562914288,23.36675,41.2193032636084));
#108821=CARTESIAN_POINT('Ctrl Pts',(109.941043992756,23.36675,41.2131246434118));
#108822=CARTESIAN_POINT('Ctrl Pts',(109.966799726391,23.36675,41.2081768283695));
#108823=CARTESIAN_POINT('Ctrl Pts',(109.992794303592,23.36675,41.2044543970879));
#108824=CARTESIAN_POINT('Ctrl Pts',(110.001231861349,23.36675,41.2032461362768));
#108825=CARTESIAN_POINT('Ctrl Pts',(110.009690500122,23.36675,41.20216776691));
#108826=CARTESIAN_POINT('Ctrl Pts',(110.0181571196,23.36675,41.2012197872153));
#108827=CARTESIAN_POINT('Ctrl Pts',(110.055685764639,23.36675,41.1970178275597));
#108828=CARTESIAN_POINT('Ctrl Pts',(110.093422889363,23.36675,41.1953662362226));
#108829=CARTESIAN_POINT('Ctrl Pts',(110.131060990144,23.36675,41.1962158968578));
#108830=CARTESIAN_POINT('Ctrl Pts',(110.168976618814,23.36675,41.1970718225414));
#108831=CARTESIAN_POINT('Ctrl Pts',(110.206793073989,23.36675,41.2004656411429));
#108832=CARTESIAN_POINT('Ctrl Pts',(110.244219876593,23.36675,41.2063948015286));
#108833=CARTESIAN_POINT('Ctrl Pts',(110.264234048366,23.36675,41.2095654499991));
#108834=CARTESIAN_POINT('Ctrl Pts',(110.284137081409,23.36675,41.2134619553918));
#108835=CARTESIAN_POINT('Ctrl Pts',(110.303885271042,23.36675,41.2180900338887));
#108836=CARTESIAN_POINT('Ctrl Pts',(110.311643364417,23.36675,41.2199081785287));
#108837=CARTESIAN_POINT('Ctrl Pts',(110.31937791337,23.36675,41.2218395140319));
#108838=CARTESIAN_POINT('Ctrl Pts',(110.327071396012,23.36675,41.2238802066803));
#108839=CARTESIAN_POINT('Ctrl Pts',(110.366741777769,23.36675,41.2344027567634));
#108840=CARTESIAN_POINT('Ctrl Pts',(110.405415001551,23.36675,41.2478495563126));
#108841=CARTESIAN_POINT('Ctrl Pts',(110.442737999354,23.36675,41.2641904381727));
#108842=CARTESIAN_POINT('Ctrl Pts',(110.477160799849,23.36675,41.2792615457821));
#108843=CARTESIAN_POINT('Ctrl Pts',(110.510436743391,23.36675,41.2967944343093));
#108844=CARTESIAN_POINT('Ctrl Pts',(110.542458466816,23.36675,41.3165519498535));
#108845=CARTESIAN_POINT('Ctrl Pts',(110.557087770437,23.36675,41.3255782814429));
#108846=CARTESIAN_POINT('Ctrl Pts',(110.57145516249,23.36675,41.3350696364183));
#108847=CARTESIAN_POINT('Ctrl Pts',(110.585549426311,23.36675,41.3450067176969));
#108848=CARTESIAN_POINT('Ctrl Pts',(110.592366803798,23.36675,41.3498132712743));
#108849=CARTESIAN_POINT('Ctrl Pts',(110.599120267254,23.36675,41.3547241379346));
#108850=CARTESIAN_POINT('Ctrl Pts',(110.605808473246,23.36675,41.3597372899822));
#108851=CARTESIAN_POINT('Ctrl Pts',(110.612060773751,23.36675,41.3644237085989));
#108852=CARTESIAN_POINT('Ctrl Pts',(110.618252318128,23.36675,41.3691968134977));
#108853=CARTESIAN_POINT('Ctrl Pts',(110.624375787699,23.36675,41.3740493717938));
#108854=CARTESIAN_POINT('Ctrl Pts',(110.655391774354,23.36675,41.3986280655561));
#108855=CARTESIAN_POINT('Ctrl Pts',(110.684712587694,23.36675,41.4252784641286));
#108856=CARTESIAN_POINT('Ctrl Pts',(110.712226150003,23.36675,41.4537232719963));
#108857=CARTESIAN_POINT('Ctrl Pts',(110.740390836705,23.36675,41.4828412427224));
#108858=CARTESIAN_POINT('Ctrl Pts',(110.766662646556,23.36675,41.5138401512147));
#108859=CARTESIAN_POINT('Ctrl Pts',(110.790902143872,23.36675,41.5464736475016));
#108860=CARTESIAN_POINT('Ctrl Pts',(110.802327249331,23.36675,41.5618552014886));
#108861=CARTESIAN_POINT('Ctrl Pts',(110.813300488072,23.36675,41.5776005713721));
#108862=CARTESIAN_POINT('Ctrl Pts',(110.823804900303,23.36675,41.5936871406374));
#108863=CARTESIAN_POINT('Ctrl Pts',(110.829218563341,23.36675,41.6019776821278));
#108864=CARTESIAN_POINT('Ctrl Pts',(110.834507674679,23.36675,41.6103588780924));
#108865=CARTESIAN_POINT('Ctrl Pts',(110.839669716296,23.36675,41.6188278067615));
#108866=CARTESIAN_POINT('Ctrl Pts',(110.844131071638,23.36675,41.6261471782345));
#108867=CARTESIAN_POINT('Ctrl Pts',(110.848493088426,23.36675,41.6335249163995));
#108868=CARTESIAN_POINT('Ctrl Pts',(110.852752219124,23.36675,41.6409543603531));
#108869=CARTESIAN_POINT('Ctrl Pts',(110.873798952144,23.36675,41.6776673739833));
#108870=CARTESIAN_POINT('Ctrl Pts',(110.892355271488,23.36675,41.7156717003438));
#108871=CARTESIAN_POINT('Ctrl Pts',(110.90828352324,23.36675,41.7546923358551));
#108872=CARTESIAN_POINT('Ctrl Pts',(110.924103863858,23.36675,41.7934486133495));
#108873=CARTESIAN_POINT('Ctrl Pts',(110.937332486947,23.36675,41.8332084462172));
#108874=CARTESIAN_POINT('Ctrl Pts',(110.947800034903,23.36675,41.8737389314944));
#108875=CARTESIAN_POINT('Ctrl Pts',(110.955324313756,23.36675,41.9028730395555));
#108876=CARTESIAN_POINT('Ctrl Pts',(110.961421269866,23.36675,41.9324061480694));
#108877=CARTESIAN_POINT('Ctrl Pts',(110.966013043313,23.36675,41.9622592706773));
#108878=CARTESIAN_POINT('',(109.03325,23.36675,42.));
#108879=CARTESIAN_POINT('Origin',(110.,23.36675,42.));
#108880=CARTESIAN_POINT('',(110.622527742627,23.36675,42.7406037150629));
#108881=CARTESIAN_POINT('Origin',(110.,23.36675,42.));
#108882=CARTESIAN_POINT('Ctrl Pts',(110.622830835844,23.36675,42.7413141620339));
#108883=CARTESIAN_POINT('Ctrl Pts',(110.599989634549,23.36675,42.7566319918816));
#108884=CARTESIAN_POINT('Ctrl Pts',(110.576498629828,23.36675,42.77088175598));
#108885=CARTESIAN_POINT('Ctrl Pts',(110.552388008497,23.36675,42.7839885195071));
#108886=CARTESIAN_POINT('Ctrl Pts',(110.519529732011,23.36675,42.8018505917406));
#108887=CARTESIAN_POINT('Ctrl Pts',(110.485520388848,23.36675,42.817590950745));
#108888=CARTESIAN_POINT('Ctrl Pts',(110.450577637721,23.36675,42.8312003669318));
#108889=CARTESIAN_POINT('Ctrl Pts',(110.435562109163,23.36675,42.8370485778143));
#108890=CARTESIAN_POINT('Ctrl Pts',(110.420374190204,23.36675,42.8425028947487));
#108891=CARTESIAN_POINT('Ctrl Pts',(110.405031249077,23.36675,42.8475608039096));
#108892=CARTESIAN_POINT('Ctrl Pts',(110.394627168308,23.36675,42.8509905827894));
#108893=CARTESIAN_POINT('Ctrl Pts',(110.384150292893,23.36675,42.8542383301765));
#108894=CARTESIAN_POINT('Ctrl Pts',(110.373624138033,23.36675,42.8572982649821));
#108895=CARTESIAN_POINT('Ctrl Pts',(110.333558504764,23.36675,42.8689452744911));
#108896=CARTESIAN_POINT('Ctrl Pts',(110.292721046436,23.36675,42.8778954764353));
#108897=CARTESIAN_POINT('Ctrl Pts',(110.251418895275,23.36675,42.8841357112893));
#108898=CARTESIAN_POINT('Ctrl Pts',(110.227354637757,23.36675,42.8877715175191));
#108899=CARTESIAN_POINT('Ctrl Pts',(110.203132624234,23.36675,42.8904863918268));
#108900=CARTESIAN_POINT('Ctrl Pts',(110.178815468667,23.36675,42.8922697532124));
#108901=CARTESIAN_POINT('Ctrl Pts',(110.168535476505,23.36675,42.8930236629784));
#108902=CARTESIAN_POINT('Ctrl Pts',(110.158238509494,23.36675,42.8936110274913));
#108903=CARTESIAN_POINT('Ctrl Pts',(110.147929448515,23.36675,42.894030741929));
#108904=CARTESIAN_POINT('Ctrl Pts',(110.139394679409,23.36675,42.8943782193398));
#108905=CARTESIAN_POINT('Ctrl Pts',(110.130860584535,23.36675,42.8946104043804));
#108906=CARTESIAN_POINT('Ctrl Pts',(110.122331803943,23.36675,42.8947273289625));
#108907=CARTESIAN_POINT('Ctrl Pts',(110.082232323714,23.36675,42.8952770693291));
#108908=CARTESIAN_POINT('Ctrl Pts',(110.042234507434,23.36675,42.8932833778413));
#108909=CARTESIAN_POINT('Ctrl Pts',(110.002614476038,23.36675,42.8887284438273));
#108910=CARTESIAN_POINT('Ctrl Pts',(109.96391576674,23.36675,42.8842794300059));
#108911=CARTESIAN_POINT('Ctrl Pts',(109.925576454932,23.36675,42.8773865373935));
#108912=CARTESIAN_POINT('Ctrl Pts',(109.88787553385,23.36675,42.8679900813404));
#108913=CARTESIAN_POINT('Ctrl Pts',(109.869444813718,23.36675,42.8633964680603));
#108914=CARTESIAN_POINT('Ctrl Pts',(109.851167090035,23.36675,42.8582038996012));
#108915=CARTESIAN_POINT('Ctrl Pts',(109.833077994259,23.36675,42.8524019136406));
#108916=CARTESIAN_POINT('Ctrl Pts',(109.825786637571,23.36675,42.8500632478684));
#108917=CARTESIAN_POINT('Ctrl Pts',(109.818525954487,23.36675,42.8476255425698));
#108918=CARTESIAN_POINT('Ctrl Pts',(109.811298392462,23.36675,42.8450880116248));
#108919=CARTESIAN_POINT('Ctrl Pts',(109.80372490632,23.36675,42.8424290298855));
#108920=CARTESIAN_POINT('Ctrl Pts',(109.79619589683,23.36675,42.8396632494703));
#108921=CARTESIAN_POINT('Ctrl Pts',(109.788717112427,23.36675,42.8367917024267));
#108922=CARTESIAN_POINT('Ctrl Pts',(109.754009543215,23.36675,42.823465416711));
#108923=CARTESIAN_POINT('Ctrl Pts',(109.720357321898,23.36675,42.8078559975844));
#108924=CARTESIAN_POINT('Ctrl Pts',(109.6880062221,23.36675,42.7899211270859));
#108925=CARTESIAN_POINT('Ctrl Pts',(109.657136500616,23.36675,42.7728075062018));
#108926=CARTESIAN_POINT('Ctrl Pts',(109.627451293261,23.36675,42.7535752657674));
#108927=CARTESIAN_POINT('Ctrl Pts',(109.599088885777,23.36675,42.7324037129303));
#108928=CARTESIAN_POINT('Ctrl Pts',(109.584394257825,23.36675,42.7214346831588));
#108929=CARTESIAN_POINT('Ctrl Pts',(109.570055217726,23.36675,42.7099447409629));
#108930=CARTESIAN_POINT('Ctrl Pts',(109.556094587763,23.36675,42.6979572564491));
#108931=CARTESIAN_POINT('Ctrl Pts',(109.549550462915,23.36675,42.692338054774));
#108932=CARTESIAN_POINT('Ctrl Pts',(109.543089524179,23.36675,42.6866095167489));
#108933=CARTESIAN_POINT('Ctrl Pts',(109.536714326725,23.36675,42.6807740087885));
#108934=CARTESIAN_POINT('Ctrl Pts',(109.531161622462,23.36675,42.6756913662265));
#108935=CARTESIAN_POINT('Ctrl Pts',(109.525677396191,23.36675,42.6705306180132));
#108936=CARTESIAN_POINT('Ctrl Pts',(109.52026864601,23.36675,42.6652991990941));
#108937=CARTESIAN_POINT('Ctrl Pts',(109.493456603764,23.36675,42.6393662163564));
#108938=CARTESIAN_POINT('Ctrl Pts',(109.468451235971,23.36675,42.6116582827426));
#108939=CARTESIAN_POINT('Ctrl Pts',(109.445404251841,23.36675,42.5824010814883));
#108940=CARTESIAN_POINT('Ctrl Pts',(109.422626821305,23.36675,42.5534860674685));
#108941=CARTESIAN_POINT('Ctrl Pts',(109.401761820652,23.36675,42.5230565668517));
#108942=CARTESIAN_POINT('Ctrl Pts',(109.3830039642,23.36675,42.4913162448205));
#108943=CARTESIAN_POINT('Ctrl Pts',(109.374367167512,23.36675,42.4767018506383));
#108944=CARTESIAN_POINT('Ctrl Pts',(109.366177803065,23.36675,42.4618094753382));
#108945=CARTESIAN_POINT('Ctrl Pts',(109.358458731183,23.36675,42.4466590557636));
#108946=CARTESIAN_POINT('Ctrl Pts',(109.353454535735,23.36675,42.4368371935207));
#108947=CARTESIAN_POINT('Ctrl Pts',(109.348645687868,23.36675,42.4269012311359));
#108948=CARTESIAN_POINT('Ctrl Pts',(109.344052541533,23.36675,42.4168877708613));
#108949=CARTESIAN_POINT('Ctrl Pts',(109.329326840271,23.36675,42.3847844556495));
#108950=CARTESIAN_POINT('Ctrl Pts',(109.316787386093,23.36675,42.351837783171));
#108951=CARTESIAN_POINT('Ctrl Pts',(109.306593405068,23.36675,42.318236792011));
#108952=CARTESIAN_POINT('Ctrl Pts',(109.296770659685,23.36675,42.2858594528769));
#108953=CARTESIAN_POINT('Ctrl Pts',(109.289125656932,23.36675,42.2528736472171));
#108954=CARTESIAN_POINT('Ctrl Pts',(109.283848189441,23.36675,42.219452110081));
#108955=CARTESIAN_POINT('Ctrl Pts',(109.280227872688,23.36675,42.1965250999214));
#108956=CARTESIAN_POINT('Ctrl Pts',(109.277722664731,23.36675,42.1733931203794));
#108957=CARTESIAN_POINT('Ctrl Pts',(109.276407492811,23.36675,42.1501162334309));
#108958=CARTESIAN_POINT('Ctrl Pts',(109.675031770393,25.824741523808,42.6637142832168));
#108959=CARTESIAN_POINT('Ctrl Pts',(109.456005826793,25.8037330492455,42.5564746547661));
#108960=CARTESIAN_POINT('Ctrl Pts',(109.136184530949,25.7617161001206,42.1096717045468));
#108961=CARTESIAN_POINT('Ctrl Pts',(109.434256215294,25.6986906764332,41.3367908296269));
#108962=CARTESIAN_POINT('Ctrl Pts',(110.244029991095,25.6356652527458,41.163702727801));
#108963=CARTESIAN_POINT('Ctrl Pts',(110.833061721015,25.5726398290584,41.7448763929315));
#108964=CARTESIAN_POINT('Ctrl Pts',(110.670381733412,25.509614405371,42.5566073819969));
#108965=CARTESIAN_POINT('Ctrl Pts',(109.902492493296,25.4465889816836,42.8657999717889));
#108966=CARTESIAN_POINT('Ctrl Pts',(109.222666943948,25.3835635579963,42.3935651416645));
#108967=CARTESIAN_POINT('Ctrl Pts',(109.244454999697,25.3205381343089,41.5660599805031));
#108968=CARTESIAN_POINT('Ctrl Pts',(109.948226154444,25.2575127106215,41.130252762051));
#108969=CARTESIAN_POINT('Ctrl Pts',(110.698724042524,25.1944872869341,41.479491846189));
#108970=CARTESIAN_POINT('Ctrl Pts',(110.818540825836,25.1314618632468,42.298556232552));
#108971=CARTESIAN_POINT('Ctrl Pts',(110.19952340274,25.0684364395593,42.8481356795978));
#108972=CARTESIAN_POINT('Ctrl Pts',(109.400412348972,25.005411015872,42.632169904582));
#108973=CARTESIAN_POINT('Ctrl Pts',(109.142502032814,24.9423855921846,41.8455933143042));
#108974=CARTESIAN_POINT('Ctrl Pts',(109.658588394334,24.8793601684972,41.1983877597661));
#108975=CARTESIAN_POINT('Ctrl Pts',(110.482840325691,24.8163347448098,41.2747349865707));
#108976=CARTESIAN_POINT('Ctrl Pts',(110.871269977697,24.7533093211224,42.0057224200596));
#108977=CARTESIAN_POINT('Ctrl Pts',(110.473272149655,24.6902838974351,42.7315446535164));
#108978=CARTESIAN_POINT('Ctrl Pts',(109.64808846612,24.6272584737477,42.7970585845476));
#108979=CARTESIAN_POINT('Ctrl Pts',(109.140547876918,24.5642330500603,42.1431298816027));
#108980=CARTESIAN_POINT('Ctrl Pts',(109.408767702043,24.5012076263729,41.3600090019544));
#108981=CARTESIAN_POINT('Ctrl Pts',(110.210646810159,24.4381822026855,41.1545580791696));
#108982=CARTESIAN_POINT('Ctrl Pts',(110.822391482929,24.3751567789981,41.7122216675569));
#108983=CARTESIAN_POINT('Ctrl Pts',(110.691827467654,24.3121313553108,42.5296402771459));
#108984=CARTESIAN_POINT('Ctrl Pts',(109.93680480607,24.2491059316234,42.8689939906469));
#108985=CARTESIAN_POINT('Ctrl Pts',(109.238823394285,24.186080507936,42.4239744266317));
#108986=CARTESIAN_POINT('Ctrl Pts',(109.227897007069,24.1230550842486,41.5962665637389));
#108987=CARTESIAN_POINT('Ctrl Pts',(109.913887232595,24.0600296605612,41.1329766445788));
#108988=CARTESIAN_POINT('Ctrl Pts',(110.677605894697,23.9970042368739,41.452282666646));
#108989=CARTESIAN_POINT('Ctrl Pts',(110.82970011946,23.9339788131865,42.2659671046784));
#108990=CARTESIAN_POINT('Ctrl Pts',(110.232893883192,23.8709533894991,42.839590749815));
#108991=CARTESIAN_POINT('Ctrl Pts',(109.425861680241,23.8079279658117,42.6553666077465));
#108992=CARTESIAN_POINT('Ctrl Pts',(109.137082167534,23.7449025421243,41.8796250880568));
#108993=CARTESIAN_POINT('Ctrl Pts',(109.627143274457,23.6818771184369,41.2124713920096));
#108994=CARTESIAN_POINT('Ctrl Pts',(110.453854470857,23.6188516947496,41.2562957542224));
#108995=CARTESIAN_POINT('Ctrl Pts',(110.870694764692,23.5558262710622,41.9711141768508));
#108996=CARTESIAN_POINT('Ctrl Pts',(110.502088724856,23.4928008473748,42.7126144441227));
#108997=CARTESIAN_POINT('Ctrl Pts',(109.679417589571,23.4297754236874,42.8095875279876));
#108998=CARTESIAN_POINT('Ctrl Pts',(109.325945901895,23.3877584745625,42.3889020117039));
#108999=CARTESIAN_POINT('Ctrl Pts',(109.276407492811,23.36675,42.1501162334309));
#109000=CARTESIAN_POINT('Ctrl Pts',(109.641648137424,25.780911015872,42.731896930038));
#109001=CARTESIAN_POINT('Ctrl Pts',(109.400121896731,25.7599025413095,42.6136406911319));
#109002=CARTESIAN_POINT('Ctrl Pts',(109.047445706828,25.7178855921846,42.1209381595358));
#109003=CARTESIAN_POINT('Ctrl Pts',(109.376137971286,25.6548601684972,41.268660072499));
#109004=CARTESIAN_POINT('Ctrl Pts',(110.269098926806,25.5918347448098,41.0777908181288));
#109005=CARTESIAN_POINT('Ctrl Pts',(110.918641246031,25.5288093211224,41.7186678221105));
#109006=CARTESIAN_POINT('Ctrl Pts',(110.739249320144,25.4657838974351,42.6137870532869));
#109007=CARTESIAN_POINT('Ctrl Pts',(109.892475653128,25.4027584737477,42.954742661719));
#109008=CARTESIAN_POINT('Ctrl Pts',(109.142812364103,25.3397330500603,42.4339956608409));
#109009=CARTESIAN_POINT('Ctrl Pts',(109.166838683135,25.2767076263729,41.5214817940167));
#109010=CARTESIAN_POINT('Ctrl Pts',(109.942907483571,25.2136822026855,41.0409045737592));
#109011=CARTESIAN_POINT('Ctrl Pts',(110.770503203861,25.1506567789981,41.4260206093688));
#109012=CARTESIAN_POINT('Ctrl Pts',(110.902628635076,25.0876313553108,42.3292265897751));
#109013=CARTESIAN_POINT('Ctrl Pts',(110.22002022501,25.0246059316234,42.9352637359931));
#109014=CARTESIAN_POINT('Ctrl Pts',(109.338817361366,24.961580507936,42.6971120316765));
#109015=CARTESIAN_POINT('Ctrl Pts',(109.054412198792,24.8985550842486,41.8297312833312));
#109016=CARTESIAN_POINT('Ctrl Pts',(109.623515551217,24.8355296605612,41.1160390057232));
#109017=CARTESIAN_POINT('Ctrl Pts',(110.532441987476,24.7725042368739,41.2002293001437));
#109018=CARTESIAN_POINT('Ctrl Pts',(110.960774595388,24.7094788131865,42.0063102780518));
#109019=CARTESIAN_POINT('Ctrl Pts',(110.521890883116,24.6464533894991,42.8066954405431));
#109020=CARTESIAN_POINT('Ctrl Pts',(109.611936976792,24.5834279658117,42.8789395464919));
#109021=CARTESIAN_POINT('Ctrl Pts',(109.052257294585,24.5204025421243,42.1578334587498));
#109022=CARTESIAN_POINT('Ctrl Pts',(109.348031050775,24.4573771184369,41.2942634224304));
#109023=CARTESIAN_POINT('Ctrl Pts',(110.232286327982,24.3943516947496,41.0677067496842));
#109024=CARTESIAN_POINT('Ctrl Pts',(110.906874865986,24.3313262710621,41.6826585122958));
#109025=CARTESIAN_POINT('Ctrl Pts',(110.762898151352,24.2683008473748,42.5840496470692));
#109026=CARTESIAN_POINT('Ctrl Pts',(109.930312832495,24.2052754236874,42.9582647986622));
#109027=CARTESIAN_POINT('Ctrl Pts',(109.160628549021,24.14225,42.4675288585962));
#109028=CARTESIAN_POINT('Ctrl Pts',(109.148579705924,24.0792245763127,41.554791466712));
#109029=CARTESIAN_POINT('Ctrl Pts',(109.905040961609,24.0161991526252,41.0439082777781));
#109030=CARTESIAN_POINT('Ctrl Pts',(110.747215611665,23.9531737289379,41.3960162603891));
#109031=CARTESIAN_POINT('Ctrl Pts',(110.914934310803,23.8901483052505,42.2932896162213));
#109032=CARTESIAN_POINT('Ctrl Pts',(110.256818818644,23.8271228815631,42.9258409948626));
#109033=CARTESIAN_POINT('Ctrl Pts',(109.366881074771,23.7640974578757,42.722691706941));
#109034=CARTESIAN_POINT('Ctrl Pts',(109.048435556643,23.7010720341883,41.867259104207));
#109035=CARTESIAN_POINT('Ctrl Pts',(109.588840108358,23.638046610501,41.1315694341973));
#109036=CARTESIAN_POINT('Ctrl Pts',(110.500478447283,23.5750211868136,41.1798958255007));
#109037=CARTESIAN_POINT('Ctrl Pts',(110.960140291376,23.5119957631262,41.9681467676392));
#109038=CARTESIAN_POINT('Ctrl Pts',(110.553667753763,23.4489703394388,42.7858205513166));
#109039=CARTESIAN_POINT('Ctrl Pts',(109.646484507038,23.3859449157514,42.892755574672));
#109040=CARTESIAN_POINT('Ctrl Pts',(109.25670105713,23.3439279666265,42.4288534926085));
#109041=CARTESIAN_POINT('Ctrl Pts',(109.202073621132,23.322919492064,42.1655375109067));
#109042=CARTESIAN_POINT('Ctrl Pts',(109.608264504454,25.737080507936,42.8000795768593));
#109043=CARTESIAN_POINT('Ctrl Pts',(109.344237966669,25.7160720333735,42.6708067274977));
#109044=CARTESIAN_POINT('Ctrl Pts',(108.958706882707,25.6740550842486,42.1322046145248));
#109045=CARTESIAN_POINT('Ctrl Pts',(109.318019727278,25.6110296605612,41.2005293153711));
#109046=CARTESIAN_POINT('Ctrl Pts',(110.294167862517,25.5480042368739,40.9918789084566));
#109047=CARTESIAN_POINT('Ctrl Pts',(111.004220771048,25.4849788131864,41.6924592512897));
#109048=CARTESIAN_POINT('Ctrl Pts',(110.808116906876,25.4219533894991,42.6709667245769));
#109049=CARTESIAN_POINT('Ctrl Pts',(109.882458812961,25.3589279658117,43.043685351649));
#109050=CARTESIAN_POINT('Ctrl Pts',(109.062957784258,25.2959025421243,42.4744261800173));
#109051=CARTESIAN_POINT('Ctrl Pts',(109.089222366572,25.2328771184369,41.4769036075303));
#109052=CARTESIAN_POINT('Ctrl Pts',(109.937588812698,25.1698516947495,40.9515563854674));
#109053=CARTESIAN_POINT('Ctrl Pts',(110.842282365199,25.1068262710622,41.3725493725486));
#109054=CARTESIAN_POINT('Ctrl Pts',(110.986716444315,25.0438008473748,42.3598969469982));
#109055=CARTESIAN_POINT('Ctrl Pts',(110.240517047281,24.9807754236874,43.0223917923884));
#109056=CARTESIAN_POINT('Ctrl Pts',(109.277222373761,24.91775,42.762054158771));
#109057=CARTESIAN_POINT('Ctrl Pts',(108.96632236477,24.8547245763126,41.8138692523581));
#109058=CARTESIAN_POINT('Ctrl Pts',(109.5884427081,24.7916991526252,41.0336902516802));
#109059=CARTESIAN_POINT('Ctrl Pts',(110.58204364926,24.7286737289379,41.1257236137168));
#109060=CARTESIAN_POINT('Ctrl Pts',(111.050279213078,24.6656483052505,42.0068981360439));
#109061=CARTESIAN_POINT('Ctrl Pts',(110.570509616578,24.6026228815631,42.8818462275699));
#109062=CARTESIAN_POINT('Ctrl Pts',(109.575785487463,24.5395974578757,42.9608205084363));
#109063=CARTESIAN_POINT('Ctrl Pts',(108.963966712252,24.4765720341883,42.1725370358968));
#109064=CARTESIAN_POINT('Ctrl Pts',(109.287294399508,24.4135466105009,41.2285178429063));
#109065=CARTESIAN_POINT('Ctrl Pts',(110.253925845805,24.3505211868136,40.9808554201988));
#109066=CARTESIAN_POINT('Ctrl Pts',(110.991358249043,24.2874957631262,41.6530953570346));
#109067=CARTESIAN_POINT('Ctrl Pts',(110.83396883505,24.2244703394388,42.6384590169925));
#109068=CARTESIAN_POINT('Ctrl Pts',(109.923820858919,24.1614449157514,43.0475356066774));
#109069=CARTESIAN_POINT('Ctrl Pts',(109.082433703756,24.098419492064,42.5110832905607));
#109070=CARTESIAN_POINT('Ctrl Pts',(109.069262404778,24.0353940683767,41.5133163696852));
#109071=CARTESIAN_POINT('Ctrl Pts',(109.896194690623,23.9723686446893,40.9548399109774));
#109072=CARTESIAN_POINT('Ctrl Pts',(110.816825328633,23.9093432210019,41.3397498541323));
#109073=CARTESIAN_POINT('Ctrl Pts',(111.000168502146,23.8463177973145,42.3206121277642));
#109074=CARTESIAN_POINT('Ctrl Pts',(110.280743754096,23.7832923736271,43.0120912399101));
#109075=CARTESIAN_POINT('Ctrl Pts',(109.307900469302,23.7202669499397,42.7900168061355));
#109076=CARTESIAN_POINT('Ctrl Pts',(108.959788945753,23.6572415262524,41.8548931203572));
#109077=CARTESIAN_POINT('Ctrl Pts',(109.550536942258,23.594216102565,41.050667476385));
#109078=CARTESIAN_POINT('Ctrl Pts',(110.54710242371,23.5311906788776,41.1034958967791));
#109079=CARTESIAN_POINT('Ctrl Pts',(111.04958581806,23.4681652551902,41.9651793584275));
#109080=CARTESIAN_POINT('Ctrl Pts',(110.605246782669,23.4051398315028,42.8590266585105));
#109081=CARTESIAN_POINT('Ctrl Pts',(109.613551424506,23.3421144078155,42.9759236213563));
#109082=CARTESIAN_POINT('Ctrl Pts',(109.187456212365,23.3000974586905,42.4688049735131));
#109083=CARTESIAN_POINT('Ctrl Pts',(109.127739749453,23.2790889841281,42.1809587883825));
#109084=CARTESIAN_POINT('Ctrl Pts',(109.574880871485,25.69325,42.8682622236805));
#109085=CARTESIAN_POINT('Ctrl Pts',(109.288354036607,25.6722415254375,42.7279727638635));
#109086=CARTESIAN_POINT('Ctrl Pts',(108.869968058586,25.6302245763126,42.1434710695137));
#109087=CARTESIAN_POINT('Ctrl Pts',(109.259901483269,25.5671991526252,41.1323985582433));
#109088=CARTESIAN_POINT('Ctrl Pts',(110.319236798229,25.5041737289379,40.9059669987843));
#109089=CARTESIAN_POINT('Ctrl Pts',(111.089800296064,25.4411483052505,41.6662506804688));
#109090=CARTESIAN_POINT('Ctrl Pts',(110.876984493608,25.3781228815631,42.7281463958668));
#109091=CARTESIAN_POINT('Ctrl Pts',(109.872441972793,25.3150974578757,43.1326280415791));
#109092=CARTESIAN_POINT('Ctrl Pts',(108.983103204413,25.2520720341883,42.5148566991937));
#109093=CARTESIAN_POINT('Ctrl Pts',(109.01160605001,25.1890466105009,41.4323254210439));
#109094=CARTESIAN_POINT('Ctrl Pts',(109.932270141825,25.1260211868136,40.8622081971757));
#109095=CARTESIAN_POINT('Ctrl Pts',(110.914061526536,25.0629957631262,41.3190781357284));
#109096=CARTESIAN_POINT('Ctrl Pts',(111.070804253555,24.9999703394388,42.3905673042213));
#109097=CARTESIAN_POINT('Ctrl Pts',(110.261013869551,24.9369449157514,43.1095198487837));
#109098=CARTESIAN_POINT('Ctrl Pts',(109.215627386155,24.873919492064,42.8269962858655));
#109099=CARTESIAN_POINT('Ctrl Pts',(108.878232530748,24.8108940683766,41.7980072213851));
#109100=CARTESIAN_POINT('Ctrl Pts',(109.553369864983,24.7478686446893,40.9513414976373));
#109101=CARTESIAN_POINT('Ctrl Pts',(110.631645311045,24.6848432210019,41.0512179272898));
#109102=CARTESIAN_POINT('Ctrl Pts',(111.139783830769,24.6218177973145,42.0074859940361));
#109103=CARTESIAN_POINT('Ctrl Pts',(110.619128350039,24.5587923736271,42.9569970145966));
#109104=CARTESIAN_POINT('Ctrl Pts',(109.539633998135,24.4957669499397,43.0427014703807));
#109105=CARTESIAN_POINT('Ctrl Pts',(108.875676129919,24.4327415262524,42.1872406130439));
#109106=CARTESIAN_POINT('Ctrl Pts',(109.22655774824,24.369716102565,41.1627722633822));
#109107=CARTESIAN_POINT('Ctrl Pts',(110.275565363628,24.3066906788776,40.8940040907134));
#109108=CARTESIAN_POINT('Ctrl Pts',(111.0758416321,24.2436652551902,41.6235322017735));
#109109=CARTESIAN_POINT('Ctrl Pts',(110.905039518748,24.1806398315029,42.6928683869158));
#109110=CARTESIAN_POINT('Ctrl Pts',(109.917328885343,24.1176144078154,43.1368064146927));
#109111=CARTESIAN_POINT('Ctrl Pts',(109.004238858492,24.0545889841281,42.5546377225252));
#109112=CARTESIAN_POINT('Ctrl Pts',(108.989945103632,23.9915635604407,41.4718412726584));
#109113=CARTESIAN_POINT('Ctrl Pts',(109.887348419636,23.9285381367533,40.8657715441766));
#109114=CARTESIAN_POINT('Ctrl Pts',(110.8864350456,23.8655127130659,41.2834834478755));
#109115=CARTESIAN_POINT('Ctrl Pts',(111.085402693489,23.8024872893785,42.347934639307));
#109116=CARTESIAN_POINT('Ctrl Pts',(110.304668689548,23.7394618656911,43.0983414849576));
#109117=CARTESIAN_POINT('Ctrl Pts',(109.248919863833,23.6764364420038,42.85734190533));
#109118=CARTESIAN_POINT('Ctrl Pts',(108.871142334862,23.6134110183164,41.8425271365074));
#109119=CARTESIAN_POINT('Ctrl Pts',(109.512233776159,23.550385594629,40.9697655185727));
#109120=CARTESIAN_POINT('Ctrl Pts',(110.593726400136,23.4873601709416,41.0270959680575));
#109121=CARTESIAN_POINT('Ctrl Pts',(111.139031344744,23.4243347472542,41.9622119492159));
#109122=CARTESIAN_POINT('Ctrl Pts',(110.656825811576,23.3613093235668,42.9322327657045));
#109123=CARTESIAN_POINT('Ctrl Pts',(109.580618341973,23.2982838998795,43.0590916680407));
#109124=CARTESIAN_POINT('Ctrl Pts',(109.1182113676,23.2562669507545,42.5087564544177));
#109125=CARTESIAN_POINT('Ctrl Pts',(109.053405877774,23.2352584761921,42.1963800658584));
#109126=CARTESIAN_POINT('Ctrl Pts',(109.032351030732,23.6222359168897,41.9993265593643));
#109127=CARTESIAN_POINT('Ctrl Pts',(109.031993297971,23.6192942840319,41.954767110875));
#109128=CARTESIAN_POINT('Ctrl Pts',(109.034808906072,23.6163526511741,41.9102527956804));
#109129=CARTESIAN_POINT('Ctrl Pts',(109.040953829907,23.6134110183164,41.8662026616554));
#109130=CARTESIAN_POINT('Ctrl Pts',(109.084839481961,23.5924025437539,41.5516065971958));
#109131=CARTESIAN_POINT('Ctrl Pts',(109.29853662906,23.5713940691915,41.2606860578843));
#109132=CARTESIAN_POINT('Ctrl Pts',(109.585633973272,23.550385594629,41.1247808631426));
#109133=CARTESIAN_POINT('Ctrl Pts',(109.872731317485,23.5293771200665,40.988875668401));
#109134=CARTESIAN_POINT('Ctrl Pts',(110.23322885881,23.5083686455041,41.0079858182292));
#109135=CARTESIAN_POINT('Ctrl Pts',(110.504361786908,23.4873601709416,41.1733935566698));
#109136=CARTESIAN_POINT('Ctrl Pts',(110.775494715005,23.4663516963791,41.3388012951103));
#109137=CARTESIAN_POINT('Ctrl Pts',(110.957263029875,23.4453432218167,41.6505066221631));
#109138=CARTESIAN_POINT('Ctrl Pts',(110.967779598448,23.4243347472542,41.9680294217709));
#109139=CARTESIAN_POINT('Ctrl Pts',(110.977388323116,23.4051398315028,42.2581420317798));
#109140=CARTESIAN_POINT('Ctrl Pts',(110.844035779942,23.3859449157514,42.5531110784096));
#109141=CARTESIAN_POINT('Ctrl Pts',(110.622830835844,23.36675,42.7413141620339));
#109142=CARTESIAN_POINT('',(109.570122622048,25.69325,41.3988956497206));
#109143=CARTESIAN_POINT('Ctrl Pts',(109.569185414382,25.69325,41.3981772519775));
#109144=CARTESIAN_POINT('Ctrl Pts',(109.550084409071,25.69325,41.4077923726575));
#109145=CARTESIAN_POINT('Ctrl Pts',(109.531472121902,25.69325,41.4182631075653));
#109146=CARTESIAN_POINT('Ctrl Pts',(109.513413199996,25.69325,41.4295739604689));
#109147=CARTESIAN_POINT('Ctrl Pts',(109.48521445685,25.69325,41.4472356922968));
#109148=CARTESIAN_POINT('Ctrl Pts',(109.45836378626,25.69325,41.4669432559766));
#109149=CARTESIAN_POINT('Ctrl Pts',(109.432922911696,25.69325,41.4884531863265));
#109150=CARTESIAN_POINT('Ctrl Pts',(109.425186378529,25.69325,41.4949943250419));
#109151=CARTESIAN_POINT('Ctrl Pts',(109.417580311137,25.69325,41.5017024633166));
#109152=CARTESIAN_POINT('Ctrl Pts',(109.410106732163,25.69325,41.5085715615065));
#109153=CARTESIAN_POINT('Ctrl Pts',(109.40357572132,25.69325,41.5145743287101));
#109154=CARTESIAN_POINT('Ctrl Pts',(109.397147155321,25.69325,41.5206990539363));
#109155=CARTESIAN_POINT('Ctrl Pts',(109.390830849284,25.69325,41.5269328221212));
#109156=CARTESIAN_POINT('Ctrl Pts',(109.365452869772,25.69325,41.5519791768034));
#109157=CARTESIAN_POINT('Ctrl Pts',(109.341846493619,25.69325,41.5788172817074));
#109158=CARTESIAN_POINT('Ctrl Pts',(109.320083986518,25.69325,41.6071642569862));
#109159=CARTESIAN_POINT('Ctrl Pts',(109.304156647206,25.69325,41.6279105750294));
#109160=CARTESIAN_POINT('Ctrl Pts',(109.289217175643,25.69325,41.6494663352333));
#109161=CARTESIAN_POINT('Ctrl Pts',(109.275301872763,25.69325,41.6717360185875));
#109162=CARTESIAN_POINT('Ctrl Pts',(109.270785129208,25.69325,41.6789644957281));
#109163=CARTESIAN_POINT('Ctrl Pts',(109.2663786605,25.69325,41.6862647740979));
#109164=CARTESIAN_POINT('Ctrl Pts',(109.262088219408,25.69325,41.6936250734435));
#109165=CARTESIAN_POINT('Ctrl Pts',(109.243070595941,25.69325,41.7262500177269));
#109166=CARTESIAN_POINT('Ctrl Pts',(109.226301260004,25.69325,41.7600968636462));
#109167=CARTESIAN_POINT('Ctrl Pts',(109.211859626931,25.69325,41.7948645052217));
#109168=CARTESIAN_POINT('Ctrl Pts',(109.197311505628,25.69325,41.8298885128565));
#109169=CARTESIAN_POINT('Ctrl Pts',(109.185124660238,25.69325,41.8658479950781));
#109170=CARTESIAN_POINT('Ctrl Pts',(109.175414211212,25.69325,41.9024762449533));
#109171=CARTESIAN_POINT('Ctrl Pts',(109.170221505687,25.69325,41.9220633634251));
#109172=CARTESIAN_POINT('Ctrl Pts',(109.16573761097,25.69325,41.9418423280385));
#109173=CARTESIAN_POINT('Ctrl Pts',(109.161985426801,25.69325,41.9617754774395));
#109174=CARTESIAN_POINT('Ctrl Pts',(109.160511365131,25.69325,41.9696063008185));
#109175=CARTESIAN_POINT('Ctrl Pts',(109.159150350403,25.69325,41.9774613586946));
#109176=CARTESIAN_POINT('Ctrl Pts',(109.157905961237,25.69325,41.9853230748385));
#109177=CARTESIAN_POINT('Ctrl Pts',(109.151489485606,25.69325,42.0258606425495));
#109178=CARTESIAN_POINT('Ctrl Pts',(109.148150748735,25.69325,42.0666685999508));
#109179=CARTESIAN_POINT('Ctrl Pts',(109.148004920988,25.69325,42.1074118288423));
#109180=CARTESIAN_POINT('Ctrl Pts',(109.14787042491,25.69325,42.1449890703042));
#109181=CARTESIAN_POINT('Ctrl Pts',(109.15045121736,25.69325,42.182512788659));
#109182=CARTESIAN_POINT('Ctrl Pts',(109.155573806821,25.69325,42.2197888984577));
#109183=CARTESIAN_POINT('Ctrl Pts',(109.157914090747,25.69325,42.2368186997458));
#109184=CARTESIAN_POINT('Ctrl Pts',(109.160785591051,25.69325,42.2537969833136));
#109185=CARTESIAN_POINT('Ctrl Pts',(109.164175193823,25.69325,42.2707056877841));
#109186=CARTESIAN_POINT('Ctrl Pts',(109.165814744614,25.69325,42.2788844277844));
#109187=CARTESIAN_POINT('Ctrl Pts',(109.167575544834,25.69325,42.2870468896487));
#109188=CARTESIAN_POINT('Ctrl Pts',(109.169456283132,25.69325,42.2951910247737));
#109189=CARTESIAN_POINT('Ctrl Pts',(109.171214441329,25.69325,42.3028043529732));
#109190=CARTESIAN_POINT('Ctrl Pts',(109.173076450049,25.69325,42.3103971639544));
#109191=CARTESIAN_POINT('Ctrl Pts',(109.175038653318,25.69325,42.3179598395574));
#109192=CARTESIAN_POINT('Ctrl Pts',(109.184977396073,25.69325,42.3562654975615));
#109193=CARTESIAN_POINT('Ctrl Pts',(109.197496367751,25.69325,42.3938584158793));
#109194=CARTESIAN_POINT('Ctrl Pts',(109.212387269368,25.69325,42.4305239662854));
#109195=CARTESIAN_POINT('Ctrl Pts',(109.227630572578,25.69325,42.4680572276404));
#109196=CARTESIAN_POINT('Ctrl Pts',(109.245359567467,25.69325,42.5046197943016));
#109197=CARTESIAN_POINT('Ctrl Pts',(109.265405320073,25.69325,42.5399845289048));
#109198=CARTESIAN_POINT('Ctrl Pts',(109.274853740721,25.69325,42.5566534410285));
#109199=CARTESIAN_POINT('Ctrl Pts',(109.284817619868,25.69325,42.573056179039));
#109200=CARTESIAN_POINT('Ctrl Pts',(109.295283129801,25.69325,42.5891680866639));
#109201=CARTESIAN_POINT('Ctrl Pts',(109.300676937784,25.69325,42.5974719855196));
#109202=CARTESIAN_POINT('Ctrl Pts',(109.306204030372,25.69325,42.6056986184729));
#109203=CARTESIAN_POINT('Ctrl Pts',(109.311862753256,25.69325,42.6138445007638));
#109204=CARTESIAN_POINT('Ctrl Pts',(109.316753006447,25.69325,42.6208841504675));
#109205=CARTESIAN_POINT('Ctrl Pts',(109.321736800868,25.69325,42.627856548227));
#109206=CARTESIAN_POINT('Ctrl Pts',(109.326809480733,25.69325,42.6347557588421));
#109207=CARTESIAN_POINT('Ctrl Pts',(109.351877367358,25.69325,42.6688498933249));
#109208=CARTESIAN_POINT('Ctrl Pts',(109.379133279473,25.69325,42.701188413472));
#109209=CARTESIAN_POINT('Ctrl Pts',(109.408381355878,25.69325,42.7315342256809));
#109210=CARTESIAN_POINT('Ctrl Pts',(109.437431291085,25.69325,42.7616744600759));
#109211=CARTESIAN_POINT('Ctrl Pts',(109.46844702927,25.69325,42.7898500743276));
#109212=CARTESIAN_POINT('Ctrl Pts',(109.501284033797,25.69325,42.8158120012212));
#109213=CARTESIAN_POINT('Ctrl Pts',(109.524887847922,25.69325,42.8344738890984));
#109214=CARTESIAN_POINT('Ctrl Pts',(109.549433713551,25.69325,42.8519916790737));
#109215=CARTESIAN_POINT('Ctrl Pts',(109.574880871485,25.69325,42.8682622236805));
#109216=CARTESIAN_POINT('Ctrl Pts',(109.569185414382,25.69325,41.3981772519775));
#109217=CARTESIAN_POINT('Ctrl Pts',(109.750509183194,25.6740550842486,41.2700703592373));
#109218=CARTESIAN_POINT('Ctrl Pts',(110.2609794001,25.6338516939347,41.1804260207118));
#109219=CARTESIAN_POINT('Ctrl Pts',(110.833061721015,25.5726398290584,41.7448763929315));
#109220=CARTESIAN_POINT('Ctrl Pts',(110.670381733412,25.509614405371,42.5566073819969));
#109221=CARTESIAN_POINT('Ctrl Pts',(109.902492493296,25.4465889816836,42.8657999717889));
#109222=CARTESIAN_POINT('Ctrl Pts',(109.341999413969,25.3946266601259,42.4764583909146));
#109223=CARTESIAN_POINT('Ctrl Pts',(109.261970584351,25.3636728131305,42.1159855729423));
#109224=CARTESIAN_POINT('Ctrl Pts',(109.262116416571,25.3537274406976,42.0001049160966));
#109225=CARTESIAN_POINT('Origin',(110.,25.69325,42.));
#109226=CARTESIAN_POINT('',(109.03325,25.69325,42.));
#109227=CARTESIAN_POINT('Origin',(110.,25.69325,42.));
#109228=CARTESIAN_POINT('Origin',(110.,25.69325,42.));
#109229=CARTESIAN_POINT('',(110.429877377952,25.69325,41.3988956497206));
#109230=CARTESIAN_POINT('Ctrl Pts',(110.426173582409,25.69325,42.8693912864046));
#109231=CARTESIAN_POINT('Ctrl Pts',(110.449419070301,25.69325,42.8546942308));
#109232=CARTESIAN_POINT('Ctrl Pts',(110.471950440779,25.69325,42.8389709957552));
#109233=CARTESIAN_POINT('Ctrl Pts',(110.493686951989,25.69325,42.822218891079));
#109234=CARTESIAN_POINT('Ctrl Pts',(110.523309759522,25.69325,42.7993888992837));
#109235=CARTESIAN_POINT('Ctrl Pts',(110.551457457952,25.69325,42.7746482345848));
#109236=CARTESIAN_POINT('Ctrl Pts',(110.578033597365,25.69325,42.74819223656));
#109237=CARTESIAN_POINT('Ctrl Pts',(110.589453845591,25.69325,42.7368236152635));
#109238=CARTESIAN_POINT('Ctrl Pts',(110.600583540201,25.69325,42.7251380560519));
#109239=CARTESIAN_POINT('Ctrl Pts',(110.611413359326,25.69325,42.7131504275406));
#109240=CARTESIAN_POINT('Ctrl Pts',(110.618757077373,25.69325,42.7050215970571));
#109241=CARTESIAN_POINT('Ctrl Pts',(110.625963742205,25.69325,42.6967525850163));
#109242=CARTESIAN_POINT('Ctrl Pts',(110.63301855821,25.69325,42.6883625609957));
#109243=CARTESIAN_POINT('Ctrl Pts',(110.659871269647,25.69325,42.6564276538559));
#109244=CARTESIAN_POINT('Ctrl Pts',(110.684569543192,25.69325,42.6226963939833));
#109245=CARTESIAN_POINT('Ctrl Pts',(110.706977156713,25.69325,42.5874443647455));
#109246=CARTESIAN_POINT('Ctrl Pts',(110.720032713102,25.69325,42.5669051468971));
#109247=CARTESIAN_POINT('Ctrl Pts',(110.732309766148,25.69325,42.5458492713409));
#109248=CARTESIAN_POINT('Ctrl Pts',(110.743773320964,25.69325,42.5243297266878));
#109249=CARTESIAN_POINT('Ctrl Pts',(110.748619502021,25.69325,42.5152324081565));
#109250=CARTESIAN_POINT('Ctrl Pts',(110.753320223074,25.69325,42.506052222641));
#109251=CARTESIAN_POINT('Ctrl Pts',(110.757872500094,25.69325,42.4967931874958));
#109252=CARTESIAN_POINT('Ctrl Pts',(110.761641280016,25.69325,42.4891277344492));
#109253=CARTESIAN_POINT('Ctrl Pts',(110.765304340218,25.69325,42.4814162803775));
#109254=CARTESIAN_POINT('Ctrl Pts',(110.768859833744,25.69325,42.4736630819417));
#109255=CARTESIAN_POINT('Ctrl Pts',(110.785576590795,25.69325,42.4372101018857));
#109256=CARTESIAN_POINT('Ctrl Pts',(110.799925999391,25.69325,42.3998216825895));
#109257=CARTESIAN_POINT('Ctrl Pts',(110.811780122533,25.69325,42.3617431637988));
#109258=CARTESIAN_POINT('Ctrl Pts',(110.82335859233,25.69325,42.3245501150637));
#109259=CARTESIAN_POINT('Ctrl Pts',(110.832556552458,25.69325,42.2866976047657));
#109260=CARTESIAN_POINT('Ctrl Pts',(110.839206606164,25.69325,42.2484166683166));
#109261=CARTESIAN_POINT('Ctrl Pts',(110.842457594823,25.69325,42.2297023998639));
#109262=CARTESIAN_POINT('Ctrl Pts',(110.845098911729,25.69325,42.2108858786613));
#109263=CARTESIAN_POINT('Ctrl Pts',(110.847106580664,25.69325,42.1919954630283));
#109264=CARTESIAN_POINT('Ctrl Pts',(110.847915830519,25.69325,42.1843811268934));
#109265=CARTESIAN_POINT('Ctrl Pts',(110.848622095913,25.69325,42.1767547989806));
#109266=CARTESIAN_POINT('Ctrl Pts',(110.849223668255,25.69325,42.169118399868));
#109267=CARTESIAN_POINT('Ctrl Pts',(110.84985403338,25.69325,42.1611165032625));
#109268=CARTESIAN_POINT('Ctrl Pts',(110.850368736194,25.69325,42.1531121018745));
#109269=CARTESIAN_POINT('Ctrl Pts',(110.850766396287,25.69325,42.1451108704563));
#109270=CARTESIAN_POINT('Ctrl Pts',(110.852611860866,25.69325,42.1079786829481));
#109271=CARTESIAN_POINT('Ctrl Pts',(110.851942434401,25.69325,42.0708885503444));
#109272=CARTESIAN_POINT('Ctrl Pts',(110.84862003613,25.69325,42.0340481470865));
#109273=CARTESIAN_POINT('Ctrl Pts',(110.845449780298,25.69325,41.9988947748077));
#109274=CARTESIAN_POINT('Ctrl Pts',(110.83986288333,25.69325,41.9639681123482));
#109275=CARTESIAN_POINT('Ctrl Pts',(110.831967424511,25.69325,41.9294671381188));
#109276=CARTESIAN_POINT('Ctrl Pts',(110.827876755529,25.69325,41.9115920445548));
#109277=CARTESIAN_POINT('Ctrl Pts',(110.823165875913,25.69325,41.8938315458871));
#109278=CARTESIAN_POINT('Ctrl Pts',(110.81784693204,25.69325,41.8762159653178));
#109279=CARTESIAN_POINT('Ctrl Pts',(110.815353851674,25.69325,41.8679592400915));
#109280=CARTESIAN_POINT('Ctrl Pts',(110.812727157518,25.69325,41.8597343826867));
#109281=CARTESIAN_POINT('Ctrl Pts',(110.809967980466,25.69325,41.8515446861299));
#109282=CARTESIAN_POINT('Ctrl Pts',(110.807564665586,25.69325,41.8444112477094));
#109283=CARTESIAN_POINT('Ctrl Pts',(110.805062231827,25.69325,41.8373088525883));
#109284=CARTESIAN_POINT('Ctrl Pts',(110.802464650691,25.69325,41.8302469111839));
#109285=CARTESIAN_POINT('Ctrl Pts',(110.789587578002,25.69325,41.795238521446));
#109286=CARTESIAN_POINT('Ctrl Pts',(110.774356602264,25.69325,41.7611648311545));
#109287=CARTESIAN_POINT('Ctrl Pts',(110.756916792691,25.69325,41.7282558485766));
#109288=CARTESIAN_POINT('Ctrl Pts',(110.739680949625,25.69325,41.6957317515235));
#109289=CARTESIAN_POINT('Ctrl Pts',(110.720286663262,25.69325,41.6643443970474));
#109290=CARTESIAN_POINT('Ctrl Pts',(110.698841475826,25.69325,41.6343542232482));
#109291=CARTESIAN_POINT('Ctrl Pts',(110.688967574082,25.69325,41.6205459956318));
#109292=CARTESIAN_POINT('Ctrl Pts',(110.678658532674,25.69325,41.6070345771449));
#109293=CARTESIAN_POINT('Ctrl Pts',(110.667923341888,25.69325,41.593848935211));
#109294=CARTESIAN_POINT('Ctrl Pts',(110.660962643681,25.69325,41.5852993643663));
#109295=CARTESIAN_POINT('Ctrl Pts',(110.653818546487,25.69325,41.5768823611315));
#109296=CARTESIAN_POINT('Ctrl Pts',(110.646516304445,25.69325,41.568631352059));
#109297=CARTESIAN_POINT('Ctrl Pts',(110.623108630693,25.69325,41.5421823618229));
#109298=CARTESIAN_POINT('Ctrl Pts',(110.598045622719,25.69325,41.5173919238667));
#109299=CARTESIAN_POINT('Ctrl Pts',(110.571435793576,25.69325,41.4944821051126));
#109300=CARTESIAN_POINT('Ctrl Pts',(110.545795023515,25.69325,41.4724066009192));
#109301=CARTESIAN_POINT('Ctrl Pts',(110.518717190311,25.69325,41.4520768475516));
#109302=CARTESIAN_POINT('Ctrl Pts',(110.490283536382,25.69325,41.433736275871));
#109303=CARTESIAN_POINT('Ctrl Pts',(110.470778285431,25.69325,41.421154795696));
#109304=CARTESIAN_POINT('Ctrl Pts',(110.450634687248,25.69325,41.4095103157974));
#109305=CARTESIAN_POINT('Ctrl Pts',(110.429877377952,25.69325,41.3988956497206));
#109306=CARTESIAN_POINT('Origin',(110.,25.69325,42.));
#109307=CARTESIAN_POINT('Origin',(110.,26.4327725593024,42.));
#109308=CARTESIAN_POINT('Ctrl Pts',(110.429877377952,25.69325,41.3988956497206));
#109309=CARTESIAN_POINT('Ctrl Pts',(110.628242021973,25.6722415254375,41.5407553335017));
#109310=CARTESIAN_POINT('Ctrl Pts',(110.870079721089,25.6302245763126,42.0341450801484));
#109311=CARTESIAN_POINT('Ctrl Pts',(110.448745988018,25.5671991526252,42.74735500798));
#109312=CARTESIAN_POINT('Ctrl Pts',(109.621520902912,25.5041737289379,42.7846640236677));
#109313=CARTESIAN_POINT('Ctrl Pts',(109.276538443787,25.4593648644969,42.3081202044508));
#109314=CARTESIAN_POINT('Ctrl Pts',(109.260025255512,25.4355644746184,42.0328501974113));
#109315=CARTESIAN_POINT('Ctrl Pts',(109.260278634324,25.4327725593024,42.0005281107854));
#109316=CARTESIAN_POINT('Ctrl Pts',(110.562359885163,25.824741523808,41.2136432603077));
#109317=CARTESIAN_POINT('Ctrl Pts',(110.821857881925,25.8037330492455,41.3992222174057));
#109318=CARTESIAN_POINT('Ctrl Pts',(111.138226752859,25.7617161001206,42.0446681410466));
#109319=CARTESIAN_POINT('Ctrl Pts',(110.587043550631,25.6986906764332,42.9776799106423));
#109320=CARTESIAN_POINT('Ctrl Pts',(109.504878664263,25.6356652527458,43.026487070204));
#109321=CARTESIAN_POINT('Ctrl Pts',(108.870105450825,25.5726398290584,42.1496388610647));
#109322=CARTESIAN_POINT('Ctrl Pts',(109.254965247123,25.509614405371,41.1373167601497));
#109323=CARTESIAN_POINT('Ctrl Pts',(110.312420586585,25.4465889816837,40.9038654413797));
#109324=CARTESIAN_POINT('Ctrl Pts',(111.087825583033,25.3835635579963,41.6597174172574));
#109325=CARTESIAN_POINT('Ctrl Pts',(110.881360229342,25.3205381343089,42.7227595686842));
#109326=CARTESIAN_POINT('Ctrl Pts',(109.879347874292,25.2575127106215,43.1334023191043));
#109327=CARTESIAN_POINT('Ctrl Pts',(108.986244409033,25.1944872869341,42.521021004801));
#109328=CARTESIAN_POINT('Ctrl Pts',(109.008176391962,25.1314618632468,41.4383499975927));
#109329=CARTESIAN_POINT('Ctrl Pts',(109.925351468358,25.0684364395594,40.8626388615017));
#109330=CARTESIAN_POINT('Ctrl Pts',(110.909905351887,25.005411015872,41.3135338816524));
#109331=CARTESIAN_POINT('Ctrl Pts',(111.073158915664,24.9423855921846,42.3840488332365));
#109332=CARTESIAN_POINT('Ctrl Pts',(110.267755477768,24.8793601684972,43.1079126153701));
#109333=CARTESIAN_POINT('Ctrl Pts',(109.220670114476,24.8163347448098,42.8317501890362));
#109334=CARTESIAN_POINT('Ctrl Pts',(108.877025034624,24.7533093211225,41.8048316749255));
#109335=CARTESIAN_POINT('Ctrl Pts',(109.547001899141,24.6902838974351,40.9540764141702));
#109336=CARTESIAN_POINT('Ctrl Pts',(110.625864816141,24.6272584737477,41.0473947979801));
#109337=CARTESIAN_POINT('Ctrl Pts',(111.13980837437,24.5642330500603,42.0005556202081));
#109338=CARTESIAN_POINT('Ctrl Pts',(110.624935792907,24.5012076263729,42.9532149188515));
#109339=CARTESIAN_POINT('Ctrl Pts',(109.545982411814,24.4381822026855,43.0454814573164));
#109340=CARTESIAN_POINT('Ctrl Pts',(108.876835288936,24.3751567789982,42.1940733862523));
#109341=CARTESIAN_POINT('Ctrl Pts',(109.221481392179,24.3121313553107,41.1674904586446));
#109342=CARTESIAN_POINT('Ctrl Pts',(110.268835473856,24.2491059316234,40.8923488579089));
#109343=CARTESIAN_POINT('Ctrl Pts',(111.073532860772,24.186080507936,41.6169978095687));
#109344=CARTESIAN_POINT('Ctrl Pts',(110.909235590793,24.1230550842486,42.6873524591346));
#109345=CARTESIAN_POINT('Ctrl Pts',(109.924242803773,24.0600296605612,43.1372887240647));
#109346=CARTESIAN_POINT('Ctrl Pts',(109.007628977691,23.9970042368738,42.5606808715683));
#109347=CARTESIAN_POINT('Ctrl Pts',(108.986753514865,23.9339788131865,41.4779949111826));
#109348=CARTESIAN_POINT('Ctrl Pts',(109.880451522268,23.8709533894991,40.8664721399706));
#109349=CARTESIAN_POINT('Ctrl Pts',(110.882067400023,23.8079279658117,41.2781178510068));
#109350=CARTESIAN_POINT('Ctrl Pts',(111.087487096344,23.7449025421243,42.3413054479614));
#109351=CARTESIAN_POINT('Ctrl Pts',(110.311364843364,23.6818771184369,43.0965177105864));
#109352=CARTESIAN_POINT('Ctrl Pts',(109.254096698422,23.6188516947495,42.8617898500753));
#109353=CARTESIAN_POINT('Ctrl Pts',(108.870308012805,23.5558262710622,41.8496109828972));
#109354=CARTESIAN_POINT('Ctrl Pts',(109.505739682273,23.4928008473748,40.9722914438752));
#109355=CARTESIAN_POINT('Ctrl Pts',(110.588140085362,23.4297754236874,41.0244762310742));
#109356=CARTESIAN_POINT('Ctrl Pts',(110.95355858955,23.3877584745625,41.643474631426));
#109357=CARTESIAN_POINT('Ctrl Pts',(110.966013043313,23.36675,41.9622592706773));
#109358=CARTESIAN_POINT('Ctrl Pts',(110.518199049426,25.780911015872,41.2753940567787));
#109359=CARTESIAN_POINT('Ctrl Pts',(110.757319261941,25.7599025413095,41.4463999227711));
#109360=CARTESIAN_POINT('Ctrl Pts',(111.048844408936,25.7178855921846,42.0411604540805));
#109361=CARTESIAN_POINT('Ctrl Pts',(110.540944363094,25.6548601684972,42.9009049430882));
#109362=CARTESIAN_POINT('Ctrl Pts',(109.54375941048,25.5918347448098,42.9458793880253));
#109363=CARTESIAN_POINT('Ctrl Pts',(108.958833485847,25.5288093211224,42.1378880635102));
#109364=CARTESIAN_POINT('Ctrl Pts',(109.313471122468,25.4657838974351,41.2050613021292));
#109365=CARTESIAN_POINT('Ctrl Pts',(110.287886912386,25.4027584737477,40.9899423815489));
#109366=CARTESIAN_POINT('Ctrl Pts',(111.002401127715,25.3397330500603,41.6864390302975));
#109367=CARTESIAN_POINT('Ctrl Pts',(110.81214902609,25.2767076263729,42.6660029126139));
#109368=CARTESIAN_POINT('Ctrl Pts',(109.888822409808,25.2136822026855,43.0443988269308));
#109369=CARTESIAN_POINT('Ctrl Pts',(109.065852317263,25.1506567789981,42.4801064168023));
#109370=CARTESIAN_POINT('Ctrl Pts',(109.086062031728,25.0876313553108,41.4824550878601));
#109371=CARTESIAN_POINT('Ctrl Pts',(109.931213446836,25.0246059316234,40.9519532307089));
#109372=CARTESIAN_POINT('Ctrl Pts',(110.838452565441,24.961580507936,41.3674404960662));
#109373=CARTESIAN_POINT('Ctrl Pts',(110.988886200194,24.8985550842486,42.353890356633));
#109374=CARTESIAN_POINT('Ctrl Pts',(110.246729252421,24.8355296605612,43.0209107713392));
#109375=CARTESIAN_POINT('Ctrl Pts',(109.281869108159,24.7725042368738,42.7664347487973));
#109376=CARTESIAN_POINT('Ctrl Pts',(108.965209690555,24.7094788131865,41.8201577971686));
#109377=CARTESIAN_POINT('Ctrl Pts',(109.582574804053,24.6464533894991,41.0362104014723));
#109378=CARTESIAN_POINT('Ctrl Pts',(110.576717083402,24.5834279658117,41.1222007060087));
#109379=CARTESIAN_POINT('Ctrl Pts',(111.050301829327,24.5204025421243,42.0005119886239));
#109380=CARTESIAN_POINT('Ctrl Pts',(110.575861014238,24.4573771184369,42.8783611311544));
#109381=CARTESIAN_POINT('Ctrl Pts',(109.581635374735,24.3943516947495,42.9633821893555));
#109382=CARTESIAN_POINT('Ctrl Pts',(108.965034845162,24.3313262710622,42.1788332470509));
#109383=CARTESIAN_POINT('Ctrl Pts',(109.282616678079,24.2683008473748,41.2328655290846));
#109384=CARTESIAN_POINT('Ctrl Pts',(110.247724438886,24.2052754236874,40.9793301690411));
#109385=CARTESIAN_POINT('Ctrl Pts',(110.989230780248,24.14225,41.6470740957064));
#109386=CARTESIAN_POINT('Ctrl Pts',(110.837835399153,24.0792245763126,42.6333762424057));
#109387=CARTESIAN_POINT('Ctrl Pts',(109.930191843146,24.0161991526253,43.0479800413974));
#109388=CARTESIAN_POINT('Ctrl Pts',(109.085557604648,23.9531737289379,42.5166518849293));
#109389=CARTESIAN_POINT('Ctrl Pts',(109.066321444178,23.8901483052505,41.5189867770486));
#109390=CARTESIAN_POINT('Ctrl Pts',(109.889839390833,23.8271228815631,40.9554854905858));
#109391=CARTESIAN_POINT('Ctrl Pts',(110.812800664274,23.7640974578757,41.3348056053153));
#109392=CARTESIAN_POINT('Ctrl Pts',(111.002089221612,23.7010720341883,42.3145035116548));
#109393=CARTESIAN_POINT('Ctrl Pts',(110.286914074266,23.638046610501,43.0104106823695));
#109394=CARTESIAN_POINT('Ctrl Pts',(109.31267077891,23.5750211868136,42.7941154639518));
#109395=CARTESIAN_POINT('Ctrl Pts',(108.959020141099,23.5119957631262,41.8614206884898));
#109396=CARTESIAN_POINT('Ctrl Pts',(109.544552814714,23.4489703394388,41.05299504655));
#109397=CARTESIAN_POINT('Ctrl Pts',(110.54195478946,23.3859449157514,41.1010818817501));
#109398=CARTESIAN_POINT('Ctrl Pts',(110.878677814179,23.3439279666265,41.6714717532923));
#109399=CARTESIAN_POINT('Ctrl Pts',(110.890154248169,23.322919492064,41.9652229638428));
#109400=CARTESIAN_POINT('Ctrl Pts',(110.474038213689,25.737080507936,41.3371448532496));
#109401=CARTESIAN_POINT('Ctrl Pts',(110.692780641957,25.7160720333735,41.4935776281364));
#109402=CARTESIAN_POINT('Ctrl Pts',(110.959462065013,25.6740550842486,42.0376527671144));
#109403=CARTESIAN_POINT('Ctrl Pts',(110.494845175556,25.6110296605612,42.8241299755341));
#109404=CARTESIAN_POINT('Ctrl Pts',(109.582640156696,25.5480042368739,42.8652717058465));
#109405=CARTESIAN_POINT('Ctrl Pts',(109.04756152087,25.4849788131864,42.1261372659557));
#109406=CARTESIAN_POINT('Ctrl Pts',(109.371976997812,25.4219533894991,41.2728058441086));
#109407=CARTESIAN_POINT('Ctrl Pts',(110.263353238187,25.3589279658117,41.0760193217181));
#109408=CARTESIAN_POINT('Ctrl Pts',(110.916976672397,25.2959025421243,41.7131606433377));
#109409=CARTESIAN_POINT('Ctrl Pts',(110.742937822837,25.2328771184369,42.6092462565436));
#109410=CARTESIAN_POINT('Ctrl Pts',(109.898296945324,25.1698516947496,42.9553953347574));
#109411=CARTESIAN_POINT('Ctrl Pts',(109.145460225492,25.1068262710622,42.4391918288035));
#109412=CARTESIAN_POINT('Ctrl Pts',(109.163947671494,25.0438008473748,41.5265601781276));
#109413=CARTESIAN_POINT('Ctrl Pts',(109.937075425314,24.9807754236874,41.041267599916));
#109414=CARTESIAN_POINT('Ctrl Pts',(110.766999778994,24.91775,41.42134711048));
#109415=CARTESIAN_POINT('Ctrl Pts',(110.904613484723,24.8547245763126,42.3237318800293));
#109416=CARTESIAN_POINT('Ctrl Pts',(110.225703027074,24.7916991526253,42.9339089273083));
#109417=CARTESIAN_POINT('Ctrl Pts',(109.343068101842,24.7286737289379,42.7011193085583));
#109418=CARTESIAN_POINT('Ctrl Pts',(109.053394346486,24.6656483052505,41.8354839194118));
#109419=CARTESIAN_POINT('Ctrl Pts',(109.618147708964,24.6026228815631,41.1183443887743));
#109420=CARTESIAN_POINT('Ctrl Pts',(110.527569350663,24.5395974578757,41.1970066140373));
#109421=CARTESIAN_POINT('Ctrl Pts',(110.960795284283,24.4765720341883,42.0004683570396));
#109422=CARTESIAN_POINT('Ctrl Pts',(110.526786235569,24.4135466105009,42.8035073434574));
#109423=CARTESIAN_POINT('Ctrl Pts',(109.617288337655,24.3505211868136,42.8812829213945));
#109424=CARTESIAN_POINT('Ctrl Pts',(109.053234401388,24.2874957631262,42.1635931078495));
#109425=CARTESIAN_POINT('Ctrl Pts',(109.343751963979,24.2244703394388,41.2982405995246));
#109426=CARTESIAN_POINT('Ctrl Pts',(110.226613403917,24.1614449157514,41.0663114801734));
#109427=CARTESIAN_POINT('Ctrl Pts',(110.904928699723,24.098419492064,41.677150381844));
#109428=CARTESIAN_POINT('Ctrl Pts',(110.766435207513,24.0353940683767,42.5794000256769));
#109429=CARTESIAN_POINT('Ctrl Pts',(109.936140882519,23.9723686446893,42.9586713587301));
#109430=CARTESIAN_POINT('Ctrl Pts',(109.163486231604,23.9093432210019,42.4726228982903));
#109431=CARTESIAN_POINT('Ctrl Pts',(109.145889373491,23.8463177973145,41.5599786429147));
#109432=CARTESIAN_POINT('Ctrl Pts',(109.899227259397,23.7832923736271,41.044498841201));
#109433=CARTESIAN_POINT('Ctrl Pts',(110.743533928526,23.7202669499398,41.3914933596238));
#109434=CARTESIAN_POINT('Ctrl Pts',(110.91669134688,23.6572415262523,42.2877015753482));
#109435=CARTESIAN_POINT('Ctrl Pts',(110.262463305168,23.594216102565,42.9243036541526));
#109436=CARTESIAN_POINT('Ctrl Pts',(109.371244859398,23.5311906788776,42.7264410778283));
#109437=CARTESIAN_POINT('Ctrl Pts',(109.047732269392,23.4681652551902,41.8732303940826));
#109438=CARTESIAN_POINT('Ctrl Pts',(109.583365947155,23.4051398315028,41.1336986492247));
#109439=CARTESIAN_POINT('Ctrl Pts',(110.495769493557,23.3421144078154,41.177687532426));
#109440=CARTESIAN_POINT('Ctrl Pts',(110.803797038808,23.3000974586905,41.6994688751586));
#109441=CARTESIAN_POINT('Ctrl Pts',(110.814295453026,23.2790889841281,41.9681866570083));
#109442=CARTESIAN_POINT('Ctrl Pts',(110.429877377952,25.69325,41.3988956497206));
#109443=CARTESIAN_POINT('Ctrl Pts',(110.628242021973,25.6722415254375,41.5407553335017));
#109444=CARTESIAN_POINT('Ctrl Pts',(110.870079721089,25.6302245763126,42.0341450801484));
#109445=CARTESIAN_POINT('Ctrl Pts',(110.448745988018,25.5671991526252,42.74735500798));
#109446=CARTESIAN_POINT('Ctrl Pts',(109.621520902912,25.5041737289379,42.7846640236677));
#109447=CARTESIAN_POINT('Ctrl Pts',(109.136289555893,25.4411483052505,42.1143864684012));
#109448=CARTESIAN_POINT('Ctrl Pts',(109.430482873156,25.3781228815631,41.3405503860881));
#109449=CARTESIAN_POINT('Ctrl Pts',(110.238819563989,25.3150974578757,41.1620962618873));
#109450=CARTESIAN_POINT('Ctrl Pts',(110.831552217079,25.2520720341883,41.7398822563778));
#109451=CARTESIAN_POINT('Ctrl Pts',(110.673726619585,25.1890466105009,42.5524896004734));
#109452=CARTESIAN_POINT('Ctrl Pts',(109.907771480839,25.1260211868136,42.866391842584));
#109453=CARTESIAN_POINT('Ctrl Pts',(109.225068133722,25.0629957631262,42.3982772408048));
#109454=CARTESIAN_POINT('Ctrl Pts',(109.24183331126,24.9999703394388,41.5706652683951));
#109455=CARTESIAN_POINT('Ctrl Pts',(109.942937403792,24.9369449157514,41.1305819691232));
#109456=CARTESIAN_POINT('Ctrl Pts',(110.695546992547,24.873919492064,41.4752537248938));
#109457=CARTESIAN_POINT('Ctrl Pts',(110.820340769253,24.8108940683766,42.2935734034257));
#109458=CARTESIAN_POINT('Ctrl Pts',(110.204676801728,24.7478686446893,42.8469070832775));
#109459=CARTESIAN_POINT('Ctrl Pts',(109.404267095524,24.6848432210019,42.6358038683194));
#109460=CARTESIAN_POINT('Ctrl Pts',(109.141579002417,24.6218177973145,41.850810041655));
#109461=CARTESIAN_POINT('Ctrl Pts',(109.653720613876,24.5587923736271,41.2004783760763));
#109462=CARTESIAN_POINT('Ctrl Pts',(110.478421617924,24.4957669499397,41.271812522066));
#109463=CARTESIAN_POINT('Ctrl Pts',(110.871288739239,24.4327415262524,42.0004247254552));
#109464=CARTESIAN_POINT('Ctrl Pts',(110.4777114569,24.369716102565,42.7286535557603));
#109465=CARTESIAN_POINT('Ctrl Pts',(109.652941300575,24.3066906788776,42.7991836534335));
#109466=CARTESIAN_POINT('Ctrl Pts',(109.141433957614,24.2436652551902,42.148352968648));
#109467=CARTESIAN_POINT('Ctrl Pts',(109.404887249879,24.1806398315028,41.3636156699646));
#109468=CARTESIAN_POINT('Ctrl Pts',(110.205502368947,24.1176144078154,41.1532927913056));
#109469=CARTESIAN_POINT('Ctrl Pts',(110.820626619199,24.0545889841281,41.7072266679816));
#109470=CARTESIAN_POINT('Ctrl Pts',(110.695035015874,23.9915635604407,42.525423808948));
#109471=CARTESIAN_POINT('Ctrl Pts',(109.942089921891,23.9285381367533,42.8693626760629));
#109472=CARTESIAN_POINT('Ctrl Pts',(109.241414858561,23.8655127130659,42.4285939116513));
#109473=CARTESIAN_POINT('Ctrl Pts',(109.225457302804,23.8024872893785,41.6009705087809));
#109474=CARTESIAN_POINT('Ctrl Pts',(109.908615127961,23.7394618656911,41.1335121918162));
#109475=CARTESIAN_POINT('Ctrl Pts',(110.674267192777,23.6764364420038,41.4481811139323));
#109476=CARTESIAN_POINT('Ctrl Pts',(110.831293472147,23.6134110183164,42.2608996390416));
#109477=CARTESIAN_POINT('Ctrl Pts',(110.23801253607,23.550385594629,42.8381966259357));
#109478=CARTESIAN_POINT('Ctrl Pts',(109.429818939885,23.4873601709416,42.6587666917049));
#109479=CARTESIAN_POINT('Ctrl Pts',(109.136444397686,23.4243347472542,41.8850400996752));
#109480=CARTESIAN_POINT('Ctrl Pts',(109.622179079596,23.3613093235668,41.2144022518994));
#109481=CARTESIAN_POINT('Ctrl Pts',(110.449584197655,23.2982838998795,41.254293183102));
#109482=CARTESIAN_POINT('Ctrl Pts',(110.728916263437,23.2562669507545,41.7274659970249));
#109483=CARTESIAN_POINT('Ctrl Pts',(110.738436657883,23.2352584761921,41.9711503501738));
#109484=CARTESIAN_POINT('Ctrl Pts',(110.966013043313,23.36675,41.9622592706773));
#109485=CARTESIAN_POINT('Ctrl Pts',(110.95355858955,23.3877584745625,41.643474631426));
#109486=CARTESIAN_POINT('Ctrl Pts',(110.770849337456,23.4087669491249,41.3339754312501));
#109487=CARTESIAN_POINT('Ctrl Pts',(110.499094644228,23.4297754236874,41.170528366629));
#109488=CARTESIAN_POINT('Ctrl Pts',(110.227339950999,23.4507838982499,41.0070813020079));
#109489=CARTESIAN_POINT('Ctrl Pts',(109.866539816636,23.4717923728123,40.9896863729416));
#109490=CARTESIAN_POINT('Ctrl Pts',(109.58023447121,23.4928008473748,41.1272088315787));
#109491=CARTESIAN_POINT('Ctrl Pts',(109.293929125784,23.5138093219372,41.2647312902159));
#109492=CARTESIAN_POINT('Ctrl Pts',(109.082118569294,23.5348177964997,41.5571711365565));
#109493=CARTESIAN_POINT('Ctrl Pts',(109.040178071986,23.5558262710622,41.8720875375898));
#109494=CARTESIAN_POINT('Ctrl Pts',(109.034563099285,23.5586388750782,41.9142483870906));
#109495=CARTESIAN_POINT('Ctrl Pts',(109.031992829932,23.5614514790943,41.9568121000603));
#109496=CARTESIAN_POINT('Ctrl Pts',(109.032328989546,23.5642640831103,41.9994138103573));
#109497=CARTESIAN_POINT('Origin',(110.,25.8,42.));
#109498=CARTESIAN_POINT('',(109.330384757729,25.9,42.));
#109499=CARTESIAN_POINT('Origin',(110.,25.9,42.));
#109500=CARTESIAN_POINT('',(109.480384757729,25.75,42.));
#109501=CARTESIAN_POINT('',(109.430384757729,25.8,42.));
#109502=CARTESIAN_POINT('',(109.543134871874,25.7,41.8913136141202));
#109503=CARTESIAN_POINT('Ctrl Pts',(109.543134871874,25.7,41.8913136141202));
#109504=CARTESIAN_POINT('Ctrl Pts',(109.513345646292,25.7170391114376,41.9429100663472));
#109505=CARTESIAN_POINT('Ctrl Pts',(109.480384757729,25.75,42.));
#109506=CARTESIAN_POINT('',(109.67744226472,25.7,41.6586863858798));
#109507=CARTESIAN_POINT('Origin',(110.,25.7,42.));
#109508=CARTESIAN_POINT('',(109.740192378865,25.75,41.55));
#109509=CARTESIAN_POINT('Ctrl Pts',(109.740192378865,25.75,41.55));
#109510=CARTESIAN_POINT('Ctrl Pts',(109.707231490302,25.7170391114376,41.6070899336529));
#109511=CARTESIAN_POINT('Ctrl Pts',(109.67744226472,25.7,41.6586863858798));
#109512=CARTESIAN_POINT('',(109.865692607155,25.7,41.55));
#109513=CARTESIAN_POINT('Ctrl Pts',(109.865692607155,25.7,41.55));
#109514=CARTESIAN_POINT('Ctrl Pts',(109.80611415599,25.7170391114376,41.55));
#109515=CARTESIAN_POINT('Ctrl Pts',(109.740192378865,25.75,41.55));
#109516=CARTESIAN_POINT('',(110.134307392845,25.7,41.55));
#109517=CARTESIAN_POINT('Origin',(110.,25.7,42.));
#109518=CARTESIAN_POINT('',(110.259807621135,25.75,41.55));
#109519=CARTESIAN_POINT('Ctrl Pts',(110.259807621135,25.75,41.55));
#109520=CARTESIAN_POINT('Ctrl Pts',(110.19388584401,25.7170391114376,41.55));
#109521=CARTESIAN_POINT('Ctrl Pts',(110.134307392845,25.7,41.55));
#109522=CARTESIAN_POINT('',(110.32255773528,25.7,41.6586863858798));
#109523=CARTESIAN_POINT('Ctrl Pts',(110.32255773528,25.7,41.6586863858798));
#109524=CARTESIAN_POINT('Ctrl Pts',(110.292768509698,25.7170391114376,41.6070899336528));
#109525=CARTESIAN_POINT('Ctrl Pts',(110.259807621135,25.75,41.55));
#109526=CARTESIAN_POINT('',(110.456865128126,25.7,41.8913136141202));
#109527=CARTESIAN_POINT('Origin',(110.,25.7,42.));
#109528=CARTESIAN_POINT('',(110.519615242271,25.75,42.));
#109529=CARTESIAN_POINT('Ctrl Pts',(110.519615242271,25.75,42.));
#109530=CARTESIAN_POINT('Ctrl Pts',(110.486654353708,25.7170391114376,41.9429100663472));
#109531=CARTESIAN_POINT('Ctrl Pts',(110.456865128126,25.7,41.8913136141202));
#109532=CARTESIAN_POINT('',(110.456865128126,25.7,42.1086863858798));
#109533=CARTESIAN_POINT('Ctrl Pts',(110.456865128126,25.7,42.1086863858798));
#109534=CARTESIAN_POINT('Ctrl Pts',(110.486654353708,25.7170391114376,42.0570899336529));
#109535=CARTESIAN_POINT('Ctrl Pts',(110.519615242271,25.75,42.));
#109536=CARTESIAN_POINT('',(110.32255773528,25.7,42.3413136141202));
#109537=CARTESIAN_POINT('Origin',(110.,25.7,42.));
#109538=CARTESIAN_POINT('',(110.259807621135,25.75,42.45));
#109539=CARTESIAN_POINT('Ctrl Pts',(110.259807621135,25.75,42.45));
#109540=CARTESIAN_POINT('Ctrl Pts',(110.292768509698,25.7170391114376,42.3929100663471));
#109541=CARTESIAN_POINT('Ctrl Pts',(110.32255773528,25.7,42.3413136141202));
#109542=CARTESIAN_POINT('',(110.134307392845,25.7,42.45));
#109543=CARTESIAN_POINT('Ctrl Pts',(110.134307392845,25.7,42.45));
#109544=CARTESIAN_POINT('Ctrl Pts',(110.19388584401,25.7170391114376,42.45));
#109545=CARTESIAN_POINT('Ctrl Pts',(110.259807621135,25.75,42.45));
#109546=CARTESIAN_POINT('',(109.865692607155,25.7,42.45));
#109547=CARTESIAN_POINT('Origin',(110.,25.7,42.));
#109548=CARTESIAN_POINT('',(109.740192378865,25.75,42.45));
#109549=CARTESIAN_POINT('Ctrl Pts',(109.740192378865,25.75,42.45));
#109550=CARTESIAN_POINT('Ctrl Pts',(109.80611415599,25.7170391114376,42.45));
#109551=CARTESIAN_POINT('Ctrl Pts',(109.865692607155,25.7,42.45));
#109552=CARTESIAN_POINT('',(109.67744226472,25.7,42.3413136141202));
#109553=CARTESIAN_POINT('Ctrl Pts',(109.67744226472,25.7,42.3413136141202));
#109554=CARTESIAN_POINT('Ctrl Pts',(109.707231490302,25.7170391114376,42.3929100663471));
#109555=CARTESIAN_POINT('Ctrl Pts',(109.740192378865,25.75,42.45));
#109556=CARTESIAN_POINT('',(109.543134871874,25.7,42.1086863858798));
#109557=CARTESIAN_POINT('Origin',(110.,25.7,42.));
#109558=CARTESIAN_POINT('Ctrl Pts',(109.480384757729,25.75,42.));
#109559=CARTESIAN_POINT('Ctrl Pts',(109.513345646292,25.7170391114376,42.0570899336528));
#109560=CARTESIAN_POINT('Ctrl Pts',(109.543134871874,25.7,42.1086863858798));
#109561=CARTESIAN_POINT('Origin',(110.,25.8,42.));
#109562=CARTESIAN_POINT('',(110.134307392845,25.9,41.55));
#109563=CARTESIAN_POINT('',(110.134307392845,25.8,41.55));
#109564=CARTESIAN_POINT('',(109.865692607155,25.9,41.55));
#109565=CARTESIAN_POINT('',(109.865692607155,25.8,41.55));
#109566=CARTESIAN_POINT('Origin',(110.,25.9,42.));
#109567=CARTESIAN_POINT('Origin',(110.,25.8,42.));
#109568=CARTESIAN_POINT('',(110.456865128126,25.9,41.8913136141202));
#109569=CARTESIAN_POINT('',(110.456865128126,25.8,41.8913136141202));
#109570=CARTESIAN_POINT('',(110.32255773528,25.9,41.6586863858798));
#109571=CARTESIAN_POINT('',(110.32255773528,25.8,41.6586863858798));
#109572=CARTESIAN_POINT('Origin',(110.,25.9,42.));
#109573=CARTESIAN_POINT('Origin',(110.,25.8,42.));
#109574=CARTESIAN_POINT('',(109.543134871874,25.9,41.8913136141202));
#109575=CARTESIAN_POINT('',(109.543134871874,25.8,41.8913136141202));
#109576=CARTESIAN_POINT('',(109.67744226472,25.9,41.6586863858798));
#109577=CARTESIAN_POINT('Origin',(110.,25.9,42.));
#109578=CARTESIAN_POINT('',(109.67744226472,25.8,41.6586863858798));
#109579=CARTESIAN_POINT('Origin',(110.,25.8,42.));
#109580=CARTESIAN_POINT('',(110.32255773528,25.9,42.3413136141202));
#109581=CARTESIAN_POINT('',(110.32255773528,25.8,42.3413136141202));
#109582=CARTESIAN_POINT('',(110.456865128126,25.9,42.1086863858798));
#109583=CARTESIAN_POINT('',(110.456865128126,25.8,42.1086863858798));
#109584=CARTESIAN_POINT('Origin',(110.,25.9,42.));
#109585=CARTESIAN_POINT('Origin',(110.,25.8,42.));
#109586=CARTESIAN_POINT('',(109.67744226472,25.9,42.3413136141202));
#109587=CARTESIAN_POINT('',(109.67744226472,25.8,42.3413136141202));
#109588=CARTESIAN_POINT('',(109.543134871874,25.9,42.1086863858798));
#109589=CARTESIAN_POINT('Origin',(110.,25.9,42.));
#109590=CARTESIAN_POINT('',(109.543134871874,25.8,42.1086863858798));
#109591=CARTESIAN_POINT('Origin',(110.,25.8,42.));
#109592=CARTESIAN_POINT('',(110.134307392845,25.9,42.45));
#109593=CARTESIAN_POINT('',(110.134307392845,25.8,42.45));
#109594=CARTESIAN_POINT('',(109.865692607155,25.9,42.45));
#109595=CARTESIAN_POINT('Origin',(110.,25.9,42.));
#109596=CARTESIAN_POINT('',(109.865692607155,25.8,42.45));
#109597=CARTESIAN_POINT('Origin',(110.519615242271,25.9,42.));
#109598=CARTESIAN_POINT('',(110.549663336987,25.9,41.947955173281));
#109599=CARTESIAN_POINT('',(110.519615242271,24.9,42.));
#109600=CARTESIAN_POINT('',(110.519615242271,25.9,42.));
#109601=CARTESIAN_POINT('',(110.259807621135,24.9,42.45));
#109602=CARTESIAN_POINT('',(110.519615242271,24.9,42.));
#109603=CARTESIAN_POINT('',(110.259807621135,25.9,42.45));
#109604=CARTESIAN_POINT('Origin',(110.259807621135,25.9,41.55));
#109605=CARTESIAN_POINT('',(110.419759526419,25.9,41.827044826719));
#109606=CARTESIAN_POINT('',(110.259807621135,24.9,41.55));
#109607=CARTESIAN_POINT('',(110.259807621135,25.9,41.55));
#109608=CARTESIAN_POINT('',(110.259807621135,24.9,41.55));
#109609=CARTESIAN_POINT('Origin',(109.740192378865,25.9,41.55));
#109610=CARTESIAN_POINT('',(110.250096189432,25.9,41.55));
#109611=CARTESIAN_POINT('',(109.740192378865,24.9,41.55));
#109612=CARTESIAN_POINT('',(109.740192378865,25.9,41.55));
#109613=CARTESIAN_POINT('',(109.740192378865,24.9,41.55));
#109614=CARTESIAN_POINT('Origin',(110.76,25.9,42.));
#109615=CARTESIAN_POINT('Origin',(110.76,25.9,42.));
#109616=CARTESIAN_POINT('Origin',(110.76,25.9,42.));
#109617=CARTESIAN_POINT('',(109.640336663013,25.9,41.722955173281));
#109618=CARTESIAN_POINT('Origin',(110.76,25.9,42.));
#109619=CARTESIAN_POINT('Origin',(110.76,25.9,42.));
#109620=CARTESIAN_POINT('',(109.770240473581,25.9,42.502044826719));
#109621=CARTESIAN_POINT('Origin',(110.76,25.9,42.));
#109622=CARTESIAN_POINT('',(110.509903810568,25.9,42.45));
#109623=CARTESIAN_POINT('Origin',(110.519615242271,24.9,42.));
#109624=CARTESIAN_POINT('',(109.480384757729,24.9,42.));
#109625=CARTESIAN_POINT('',(109.480384757729,24.9,42.));
#109626=CARTESIAN_POINT('Origin',(110.,24.9,42.));
#109627=CARTESIAN_POINT('Origin',(110.519615242271,24.9,42.));
#109628=CARTESIAN_POINT('Origin',(110.,24.9,42.));
#109629=CARTESIAN_POINT('Origin',(110.519615242271,24.9,42.));
#109630=CARTESIAN_POINT('Origin',(110.,24.9,42.));
#109631=CARTESIAN_POINT('Origin',(110.519615242271,24.9,42.));
#109632=CARTESIAN_POINT('Origin',(110.,24.9,42.));
#109633=CARTESIAN_POINT('Origin',(110.519615242271,24.9,42.));
#109634=CARTESIAN_POINT('',(109.740192378865,24.9,42.45));
#109635=CARTESIAN_POINT('',(110.259807621135,24.9,42.45));
#109636=CARTESIAN_POINT('Origin',(110.,24.9,42.));
#109637=CARTESIAN_POINT('Origin',(110.519615242271,24.9,42.));
#109638=CARTESIAN_POINT('',(109.740192378865,24.9,42.45));
#109639=CARTESIAN_POINT('Origin',(110.,24.9,42.));
#109640=CARTESIAN_POINT('Origin',(110.,24.9,42.));
#109641=CARTESIAN_POINT('',(110.,24.5877836638731,42.));
#109642=CARTESIAN_POINT('',(109.480384757729,24.9,42.));
#109643=CARTESIAN_POINT('Origin',(109.480384757729,25.9,42.));
#109644=CARTESIAN_POINT('',(109.480384757729,25.9,42.));
#109645=CARTESIAN_POINT('Origin',(109.740192378865,25.9,42.45));
#109646=CARTESIAN_POINT('',(109.740192378865,25.9,42.45));
#109647=CARTESIAN_POINT('Origin',(110.259807621135,25.9,42.45));
#109648=CARTESIAN_POINT('Origin',(110.76,25.9,42.));
#109649=CARTESIAN_POINT('',(109.24,25.9,42.));
#109650=CARTESIAN_POINT('Origin',(110.,25.9,42.));
#109651=CARTESIAN_POINT('Origin',(110.,25.78,42.));
#109652=CARTESIAN_POINT('',(109.12,25.78,42.));
#109653=CARTESIAN_POINT('Origin',(110.,24.53,42.));
#109654=CARTESIAN_POINT('Origin',(110.,23.36675,42.));
#109655=CARTESIAN_POINT('Origin',(110.,23.15,42.));
#109656=CARTESIAN_POINT('',(109.5,22.9,42.));
#109657=CARTESIAN_POINT('Origin',(110.,22.9,42.));
#109658=CARTESIAN_POINT('',(109.25,23.15,42.));
#109659=CARTESIAN_POINT('Origin',(110.,22.9,42.));
#113960=UNCERTAINTY_MEASURE_WITH_UNIT(LENGTH_MEASURE(0.01),#113985,
'DISTANCE_ACCURACY_VALUE',
'Maximum model space distance between geometric entities at asserted c
onnectivities');
#113964=UNCERTAINTY_MEASURE_WITH_UNIT(LENGTH_MEASURE(0.01),#113985,
'DISTANCE_ACCURACY_VALUE',
'Maximum model space distance between geometric entities at asserted c
onnectivities');
#113980=(
GEOMETRIC_REPRESENTATION_CONTEXT(3)
GLOBAL_UNCERTAINTY_ASSIGNED_CONTEXT((#113960))
GLOBAL_UNIT_ASSIGNED_CONTEXT((#113985,#113987,#113988))
REPRESENTATION_CONTEXT('','3D')
);
#113984=(
GEOMETRIC_REPRESENTATION_CONTEXT(3)
GLOBAL_UNCERTAINTY_ASSIGNED_CONTEXT((#113964))
GLOBAL_UNIT_ASSIGNED_CONTEXT((#113985,#113987,#113988))
REPRESENTATION_CONTEXT('','3D')
);
#113985=(
LENGTH_UNIT()
NAMED_UNIT(*)
SI_UNIT(.MILLI.,.METRE.)
);
#113987=(
NAMED_UNIT(*)
PLANE_ANGLE_UNIT()
SI_UNIT($,.RADIAN.)
);
#113988=(
NAMED_UNIT(*)
SI_UNIT($,.STERADIAN.)
SOLID_ANGLE_UNIT()
);
#114004=SHAPE_DEFINITION_REPRESENTATION(#114023,#114066);
#114023=PRODUCT_DEFINITION_SHAPE('',$,#114086);
#114066=SHAPE_REPRESENTATION('',(#63344),#113980);
#114070=PRODUCT_DEFINITION_CONTEXT('part definition',#114129,'design');
#114086=PRODUCT_DEFINITION('2026-10-05-09-51-36-343',
'ISO 4026 - M3 x 4 - 45H (Bush Retaining Screw)',#114105,#114070);
#114105=PRODUCT_DEFINITION_FORMATION('',$,#114146);
#114129=APPLICATION_CONTEXT(
'Core Data for Automotive Mechanical Design Process');
#114130=PRODUCT_CONTEXT('part definition',#114129,'mechanical');
#114146=PRODUCT('2026-10-05-09-51-36-343',
'ISO 4026 - M3 x 4 - 45H (Bush Retaining Screw)',$,(#114130));
#114311=COLOUR_RGB('Black',0.12,0.14,0.17);
#114312=FILL_AREA_STYLE_COLOUR('',#114311);
#114313=FILL_AREA_STYLE('',(#114312));
#114314=SURFACE_STYLE_FILL_AREA(#114313);
#114315=SURFACE_SIDE_STYLE('',(#114314));
#114316=SURFACE_STYLE_USAGE(.BOTH.,#114315);
#114317=PRESENTATION_STYLE_ASSIGNMENT((#114316));
ENDSEC;
END-ISO-10303-21;
